ISO-10303-21;
HEADER;
FILE_DESCRIPTION (('STEP AP203'),
    '1' );
FILE_NAME ('Cleco, Handle, Stationary.step',
    '2026-10-09T13:45:32',
    ( '' ),
    ( '' ),
    'SwSTEP 2.0',
    'SolidWorks 2024',
    '' );
FILE_SCHEMA (( 'AUTOMOTIVE_DESIGN' ));
ENDSEC;

DATA;
#2=SHAPE_REPRESENTATION ( 'Cleco, Handle, Stationary', ( #3555 ), #5783 ) ;
#3=DIRECTION ( 'NONE',  ( -1.000000000000000000, 0.000000000000000000, 0.000000000000000000 ) ) ;
#11=EDGE_CURVE ( 'NONE', #2855, #2155, #1899, .T. ) ;
#15=DIRECTION ( 'NONE',  ( 1.000000000000000000, 8.970601940444434686E-12, 0.000000000000000000 ) ) ;
#17=LINE ( 'NONE', #7477, #1803 ) ;
#20=ORIENTED_EDGE ( 'NONE', *, *, #5646, .T. ) ;
#22=EDGE_CURVE ( 'NONE', #963, #158, #1365, .T. ) ;
#26=FACE_OUTER_BOUND ( 'NONE', #6824, .T. ) ;
#30=LINE ( 'NONE', #3883, #1333 ) ;
#32=DIRECTION ( 'NONE',  ( -0.000000000000000000, 0.000000000000000000, 1.000000000000000000 ) ) ;
#36=CARTESIAN_POINT ( 'NONE',  ( -1.763177565995708296, 1.070083551578370207, -0.08100000000000007194 ) ) ;
#38=ORIENTED_EDGE ( 'NONE', *, *, #6492, .T. ) ;
#44=CARTESIAN_POINT ( 'NONE',  ( -1.067641779222573639, 0.6107141540073635078, 0.09374999999999998612 ) ) ;
#56=MECHANICAL_CONTEXT ( 'NONE', #1115, 'mechanical' ) ;
#57=CARTESIAN_POINT ( 'NONE',  ( 6.190221022838899856, 0.4584861219976859026, 0.1250000000000004441 ) ) ;
#58=FACE_BOUND ( 'NONE', #2776, .T. ) ;
#61=AXIS2_PLACEMENT_3D ( 'NONE', #3635, #4900, #4323 ) ;
#65=ORIENTED_EDGE ( 'NONE', *, *, #5052, .T. ) ;
#67=CYLINDRICAL_SURFACE ( 'NONE', #6771, 0.03124999999999999306 ) ;
#75=ORIENTED_EDGE ( 'NONE', *, *, #993, .T. ) ;
#76=FACE_OUTER_BOUND ( 'NONE', #4236, .T. ) ;
#81=VERTEX_POINT ( 'NONE', #6665 ) ;
#85=EDGE_LOOP ( 'NONE', ( #926, #3795, #4009, #2620 ) ) ;
#86=AXIS2_PLACEMENT_3D ( 'NONE', #7852, #2824, #5333 ) ;
#87=DIRECTION ( 'NONE',  ( -0.6568496200222107007, -0.7540216022612863389, 0.000000000000000000 ) ) ;
#91=VERTEX_POINT ( 'NONE', #2513 ) ;
#106=ORIENTED_EDGE ( 'NONE', *, *, #2026, .T. ) ;
#108=ORIENTED_EDGE ( 'NONE', *, *, #7591, .T. ) ;
#118=ORIENTED_EDGE ( 'NONE', *, *, #4536, .T. ) ;
#122=DIRECTION ( 'NONE',  ( 0.7540216022612864499, -0.6568496200222104786, 0.000000000000000000 ) ) ;
#135=DIRECTION ( 'NONE',  ( 1.000000000000000000, 0.000000000000000000, 0.000000000000000000 ) ) ;
#139=DIRECTION ( 'NONE',  ( -0.000000000000000000, 0.000000000000000000, 1.000000000000000000 ) ) ;
#142=EDGE_LOOP ( 'NONE', ( #3147, #7500, #5095 ) ) ;
#143=FACE_OUTER_BOUND ( 'NONE', #230, .T. ) ;
#146=DIRECTION ( 'NONE',  ( -0.04906492035527518919, 0.9987955914953422498, 0.000000000000000000 ) ) ;
#155=ORIENTED_EDGE ( 'NONE', *, *, #2026, .F. ) ;
#158=VERTEX_POINT ( 'NONE', #6270 ) ;
#170=EDGE_CURVE ( 'NONE', #2750, #4309, #1294, .T. ) ;
#177=LINE ( 'NONE', #220, #2975 ) ;
#189=FACE_OUTER_BOUND ( 'NONE', #317, .T. ) ;
#190=CARTESIAN_POINT ( 'NONE',  ( 1.258616367985684104, -0.02482036785324303815, 0.1849999999999999978 ) ) ;
#195=CARTESIAN_POINT ( 'NONE',  ( 4.013019369095008670, -4.147396371033809537, 0.1250000000000000000 ) ) ;
#202=DIRECTION ( 'NONE',  ( -0.8680936205257663296, 0.4964005096718443477, -0.000000000000000000 ) ) ;
#205=CARTESIAN_POINT ( 'NONE',  ( -1.983451234524918227, 1.341543513548240529, 0.1339999999999995917 ) ) ;
#208=CIRCLE ( 'NONE', #7670, 0.2515937209583817280 ) ;
#210=VECTOR ( 'NONE', #4441, 39.37007874015748143 ) ;
#213=VECTOR ( 'NONE', #4099, 39.37007874015748143 ) ;
#215=EDGE_CURVE ( 'NONE', #5845, #2895, #393, .T. ) ;
#216=ORIENTED_EDGE ( 'NONE', *, *, #4390, .T. ) ;
#220=CARTESIAN_POINT ( 'NONE',  ( -1.803041671366327314, 1.104810305277056592, 0.1649762307749162715 ) ) ;
#224=VECTOR ( 'NONE', #4772, 39.37007874015748143 ) ;
#228=ORIENTED_EDGE ( 'NONE', *, *, #6845, .T. ) ;
#230=EDGE_LOOP ( 'NONE', ( #2845, #7874, #3535, #5828 ) ) ;
#233=LINE ( 'NONE', #1455, #4810 ) ;
#235=DIRECTION ( 'NONE',  ( 0.000000000000000000, 0.000000000000000000, -1.000000000000000000 ) ) ;
#245=CARTESIAN_POINT ( 'NONE',  ( 2.387087291339119677, -6.013863021948615106, 0.1250000000000000000 ) ) ;
#258=CARTESIAN_POINT ( 'NONE',  ( -1.693021742871659407, 0.8232980029552862122, -0.08100000000000007194 ) ) ;
#265=LINE ( 'NONE', #2764, #712 ) ;
#268=DIRECTION ( 'NONE',  ( 1.000000000000000000, 4.484396833652621360E-12, 0.000000000000000000 ) ) ;
#269=CARTESIAN_POINT ( 'NONE',  ( 6.067385397437120353, 0.2407432673787524013, -0.1849999999999999978 ) ) ;
#271=EDGE_LOOP ( 'NONE', ( #4082, #3585, #738, #5261 ) ) ;
#284=CARTESIAN_POINT ( 'NONE',  ( 3.659299226295303686, -8.245510427152350275, 5.393636709996481038 ) ) ;
#289=CARTESIAN_POINT ( 'NONE',  ( 1.475891671935536609, 0.7226544316391477762, 0.09374999999999998612 ) ) ;
#297=VERTEX_POINT ( 'NONE', #794 ) ;
#298=ORIENTED_EDGE ( 'NONE', *, *, #2680, .T. ) ;
#310=DIRECTION ( 'NONE',  ( -1.000000000000000000, -9.329293658944590640E-14, 0.000000000000000000 ) ) ;
#311=FACE_OUTER_BOUND ( 'NONE', #5756, .T. ) ;
#313=AXIS2_PLACEMENT_3D ( 'NONE', #3150, #5649, #2520 ) ;
#317=EDGE_LOOP ( 'NONE', ( #5721, #5705, #2017, #5490 ) ) ;
#319=ADVANCED_FACE ( 'NONE', ( #58, #837 ), #2558, .F. ) ;
#323=CARTESIAN_POINT ( 'NONE',  ( 1.475891671935536609, 0.7226544316391472211, 0.1850000000000003586 ) ) ;
#324=EDGE_LOOP ( 'NONE', ( #5970, #4767, #1019, #404 ) ) ;
#340=VERTEX_POINT ( 'NONE', #1324 ) ;
#346=ORIENTED_EDGE ( 'NONE', *, *, #7938, .F. ) ;
#355=LINE ( 'NONE', #2313, #3850 ) ;
#356=AXIS2_PLACEMENT_3D ( 'NONE', #3356, #3430, #938 ) ;
#358=VERTEX_POINT ( 'NONE', #3220 ) ;
#359=CARTESIAN_POINT ( 'NONE',  ( 2.056298385200680201, 0.7198786976815826355, 0.09374999999999998612 ) ) ;
#364=LINE ( 'NONE', #3318, #4668 ) ;
#365=VERTEX_POINT ( 'NONE', #2023 ) ;
#373=EDGE_CURVE ( 'NONE', #1649, #2552, #3741, .T. ) ;
#375=VERTEX_POINT ( 'NONE', #759 ) ;
#378=EDGE_CURVE ( 'NONE', #845, #1086, #7789, .T. ) ;
#379=ORIENTED_EDGE ( 'NONE', *, *, #1680, .T. ) ;
#385=EDGE_LOOP ( 'NONE', ( #2646, #2923, #1441, #6335 ) ) ;
#387=ORIENTED_EDGE ( 'NONE', *, *, #7591, .F. ) ;
#390=UNCERTAINTY_MEASURE_WITH_UNIT (LENGTH_MEASURE( 1.000000000000000082E-05 ), #5132, 'distance_accuracy_value', 'NONE');
#392=DIRECTION ( 'NONE',  ( 0.9602545086670756236, -0.2791259188691606608, 0.000000000000000000 ) ) ;
#393=LINE ( 'NONE', #1746, #455 ) ;
#401=CARTESIAN_POINT ( 'NONE',  ( 3.672798492683009286, -8.252032378159654513, -0.1849999999999999978 ) ) ;
#404=ORIENTED_EDGE ( 'NONE', *, *, #6693, .F. ) ;
#406=CARTESIAN_POINT ( 'NONE',  ( 6.000000000000001776, 0.000000000000000000, -0.1849999999999999978 ) ) ;
#411=EDGE_CURVE ( 'NONE', #4769, #5004, #1009, .T. ) ;
#413=ORIENTED_EDGE ( 'NONE', *, *, #7085, .T. ) ;
#443=AXIS2_PLACEMENT_3D ( 'NONE', #6754, #1707, #2984 ) ;
#454=CARTESIAN_POINT ( 'NONE',  ( 1.466665248995881576, 0.6909135088951512405, -0.1250000000000000000 ) ) ;
#455=VECTOR ( 'NONE', #5478, 39.37007874015748143 ) ;
#456=CIRCLE ( 'NONE', #5039, 8.513908398499122399 ) ;
#463=DIRECTION ( 'NONE',  ( -1.000000000000000000, 0.000000000000000000, 0.000000000000000000 ) ) ;
#465=DIRECTION ( 'NONE',  ( 1.000000000000000000, -1.713662733658207664E-13, 0.000000000000000000 ) ) ;
#467=VECTOR ( 'NONE', #1230, 39.37007874015748143 ) ;
#469=EDGE_CURVE ( 'NONE', #1621, #2575, #7157, .T. ) ;
#470=DIRECTION ( 'NONE',  ( 1.000000000000000000, 0.000000000000000000, 0.000000000000000000 ) ) ;
#471=AXIS2_PLACEMENT_3D ( 'NONE', #5489, #2945, #5524 ) ;
#472=CARTESIAN_POINT ( 'NONE',  ( -1.411633252941551619, 0.8434166392007494961, 0.09374999999999998612 ) ) ;
#493=AXIS2_PLACEMENT_3D ( 'NONE', #3613, #5577, #1716 ) ;
#501=ORIENTED_EDGE ( 'NONE', *, *, #4788, .T. ) ;
#502=VERTEX_POINT ( 'NONE', #7802 ) ;
#503=CARTESIAN_POINT ( 'NONE',  ( 1.258671604940865274, -0.02501003737716508274, -0.1849999999999999978 ) ) ;
#509=CARTESIAN_POINT ( 'NONE',  ( 6.190219624525621356, 0.4584813330253886265, -0.1250000000000000000 ) ) ;
#517=CARTESIAN_POINT ( 'NONE',  ( 0.1743677072153199392, -0.4209564106690024676, 0.1250000000000000000 ) ) ;
#519=CARTESIAN_POINT ( 'NONE',  ( 1.258616367985684104, -0.02482036785324303815, 0.1250000000000000000 ) ) ;
#530=DIRECTION ( 'NONE',  ( 0.9602545086670756236, -0.2791259188691606608, 0.000000000000000000 ) ) ;
#532=EDGE_LOOP ( 'NONE', ( #5100, #4338, #7008, #118, #2763, #4689, #2797, #216 ) ) ;
#537=ORIENTED_EDGE ( 'NONE', *, *, #411, .T. ) ;
#545=DIRECTION ( 'NONE',  ( 1.000000000000000000, 1.942647462161253450E-15, 0.000000000000000000 ) ) ;
#551=ORIENTED_EDGE ( 'NONE', *, *, #3385, .F. ) ;
#556=DIRECTION ( 'NONE',  ( -0.2791259188691606608, -0.9602545086670756236, -0.000000000000000000 ) ) ;
#564=AXIS2_PLACEMENT_3D ( 'NONE', #1487, #6500, #5267 ) ;
#565=CARTESIAN_POINT ( 'NONE',  ( 6.191327929239395012, 0.4578608198540752294, 0.1850000000000003586 ) ) ;
#570=DIRECTION ( 'NONE',  ( -0.000000000000000000, -0.000000000000000000, 1.000000000000000000 ) ) ;
#574=CIRCLE ( 'NONE', #5153, 0.4060000000000001386 ) ;
#578=EDGE_CURVE ( 'NONE', #7112, #6856, #2382, .T. ) ;
#581=CARTESIAN_POINT ( 'NONE',  ( 6.067386035484801710, 0.2407470087491039856, 0.1250000000000000000 ) ) ;
#585=FACE_OUTER_BOUND ( 'NONE', #4092, .T. ) ;
#586=ADVANCED_FACE ( 'NONE', ( #585 ), #7958, .T. ) ;
#591=DIRECTION ( 'NONE',  ( 0.6568496200222108117, 0.7540216022612863389, -0.000000000000000000 ) ) ;
#596=VECTOR ( 'NONE', #1736, 39.37007874015748143 ) ;
#597=ORIENTED_EDGE ( 'NONE', *, *, #6829, .T. ) ;
#598=EDGE_CURVE ( 'NONE', #1607, #1086, #1853, .T. ) ;
#600=VECTOR ( 'NONE', #1687, 39.37007874015748143 ) ;
#602=CIRCLE ( 'NONE', #6366, 0.1250000000000000000 ) ;
#603=DIRECTION ( 'NONE',  ( -1.000000000000000000, 0.000000000000000000, 0.000000000000000000 ) ) ;
#605=CIRCLE ( 'NONE', #3230, 0.2499400561648078278 ) ;
#613=ORIENTED_EDGE ( 'NONE', *, *, #7841, .F. ) ;
#614=CARTESIAN_POINT ( 'NONE',  ( 6.190221022838899856, 0.4584861219976859026, -0.1250000000000004441 ) ) ;
#615=CARTESIAN_POINT ( 'NONE',  ( 3.690413561029368683, -8.374393170229348371, 0.1250000000000000000 ) ) ;
#620=FACE_OUTER_BOUND ( 'NONE', #6980, .T. ) ;
#628=DIRECTION ( 'NONE',  ( -0.8680936205257682170, 0.4964005096718413501, 0.000000000000000000 ) ) ;
#632=CARTESIAN_POINT ( 'NONE',  ( 1.356840083662244734, 0.003162463486408387866, 0.000000000000000000 ) ) ;
#633=ADVANCED_FACE ( 'NONE', ( #3581 ), #5594, .F. ) ;
#634=EDGE_CURVE ( 'NONE', #6740, #6273, #7661, .T. ) ;
#639=CARTESIAN_POINT ( 'NONE',  ( -0.9280291358773672394, 0.8548654847802351631, 0.1250000000000000000 ) ) ;
#640=DIRECTION ( 'NONE',  ( -0.000000000000000000, -0.000000000000000000, -1.000000000000000000 ) ) ;
#648=CYLINDRICAL_SURFACE ( 'NONE', #313, 0.4060000000000001386 ) ;
#649=CARTESIAN_POINT ( 'NONE',  ( -1.543211452806561912, 0.6927940070358482583, 0.1250000000000000000 ) ) ;
#652=CARTESIAN_POINT ( 'NONE',  ( 2.387087291339119677, -6.013863021948615106, 0.1250000000000000000 ) ) ;
#656=DIRECTION ( 'NONE',  ( 0.8680936205257663296, -0.4964005096718442922, 0.000000000000000000 ) ) ;
#658=VERTEX_POINT ( 'NONE', #667 ) ;
#660=DIRECTION ( 'NONE',  ( -0.000000000000000000, -0.000000000000000000, -1.000000000000000000 ) ) ;
#662=DIRECTION ( 'NONE',  ( -0.6568496200222107007, -0.7540216022612863389, 0.000000000000000000 ) ) ;
#667=CARTESIAN_POINT ( 'NONE',  ( -1.763630694164995738, 1.150051601412733771, -0.3269762307749164432 ) ) ;
#670=EDGE_CURVE ( 'NONE', #4959, #297, #4919, .T. ) ;
#671=CARTESIAN_POINT ( 'NONE',  ( -1.067641779222573639, 0.6107141540073635078, 0.1250000000000000000 ) ) ;
#672=DIRECTION ( 'NONE',  ( -1.000000000000000000, -8.862153517038291156E-15, 0.000000000000000000 ) ) ;
#675=DIRECTION ( 'NONE',  ( 1.000000000000000000, 0.000000000000000000, 0.000000000000000000 ) ) ;
#677=EDGE_LOOP ( 'NONE', ( #6726, #2915, #5765, #4975, #2876, #3002, #3508 ) ) ;
#680=CIRCLE ( 'NONE', #1199, 0.1250000000000000000 ) ;
#686=DIRECTION ( 'NONE',  ( 0.7540216022612858948, -0.6568496200222110337, 0.000000000000000000 ) ) ;
#694=AXIS2_PLACEMENT_3D ( 'NONE', #1480, #3988, #2752 ) ;
#699=ORIENTED_EDGE ( 'NONE', *, *, #6003, .F. ) ;
#700=AXIS2_PLACEMENT_3D ( 'NONE', #652, #32, #5035 ) ;
#712=VECTOR ( 'NONE', #5279, 39.37007874015748143 ) ;
#713=VERTEX_POINT ( 'NONE', #5673 ) ;
#720=VECTOR ( 'NONE', #7897, 39.37007874015748854 ) ;
#735=DIRECTION ( 'NONE',  ( 0.6568496200222108117, 0.7540216022612861169, 0.000000000000000000 ) ) ;
#736=AXIS2_PLACEMENT_3D ( 'NONE', #3557, #3024, #2446 ) ;
#738=ORIENTED_EDGE ( 'NONE', *, *, #7841, .T. ) ;
#742=AXIS2_PLACEMENT_3D ( 'NONE', #6023, #6636, #1025 ) ;
#744=AXIS2_PLACEMENT_3D ( 'NONE', #1815, #5544, #1898 ) ;
#745=CIRCLE ( 'NONE', #3110, 0.2812500000000000555 ) ;
#748=CARTESIAN_POINT ( 'NONE',  ( -1.411633252941551619, 0.8434166392007494961, -0.09374999999999998612 ) ) ;
#754=EDGE_LOOP ( 'NONE', ( #1499, #5423, #1970, #4121 ) ) ;
#758=DIRECTION ( 'NONE',  ( 0.7540216022612862279, -0.6568496200222107007, -0.000000000000000000 ) ) ;
#759=CARTESIAN_POINT ( 'NONE',  ( -1.763630694164994850, 1.150051601412733771, 0.1649762307749162715 ) ) ;
#761=VERTEX_POINT ( 'NONE', #3250 ) ;
#763=CARTESIAN_POINT ( 'NONE',  ( -1.803041671366328202, 1.104810305277057259, -0.3269762307749163877 ) ) ;
#767=DIRECTION ( 'NONE',  ( 0.000000000000000000, -0.000000000000000000, -1.000000000000000000 ) ) ;
#769=ORIENTED_EDGE ( 'NONE', *, *, #2647, .T. ) ;
#774=VERTEX_POINT ( 'NONE', #3907 ) ;
#775=PLANE ( 'NONE',  #4281 ) ;
#785=CARTESIAN_POINT ( 'NONE',  ( -1.067641779222573639, 0.6107141540073636188, -0.09374999999999998612 ) ) ;
#789=VERTEX_POINT ( 'NONE', #3789 ) ;
#794=CARTESIAN_POINT ( 'NONE',  ( -1.067641779222573639, 0.6107141540073635078, -0.1250000000000000000 ) ) ;
#796=VERTEX_POINT ( 'NONE', #6293 ) ;
#804=CYLINDRICAL_SURFACE ( 'NONE', #6206, 0.1250000000000000000 ) ;
#811=DIRECTION ( 'NONE',  ( 0.000000000000000000, 0.000000000000000000, -1.000000000000000000 ) ) ;
#813=VERTEX_POINT ( 'NONE', #5122 ) ;
#814=VECTOR ( 'NONE', #3519, 39.37007874015748143 ) ;
#815=CARTESIAN_POINT ( 'NONE',  ( 1.475891671935536609, 0.7226544316391472211, -0.1849999999999999978 ) ) ;
#816=ADVANCED_FACE ( 'NONE', ( #7623 ), #6538, .F. ) ;
#820=CARTESIAN_POINT ( 'NONE',  ( 6.185915932927993133, 0.4597367884986652831, 0.1250000000000000278 ) ) ;
#831=CIRCLE ( 'NONE', #5683, 0.2499400561648078278 ) ;
#837=FACE_OUTER_BOUND ( 'NONE', #3839, .T. ) ;
#845=VERTEX_POINT ( 'NONE', #3984 ) ;
#850=CARTESIAN_POINT ( 'NONE',  ( 3.659299226295303686, -8.245510427152350275, 0.1250000000000004441 ) ) ;
#855=AXIS2_PLACEMENT_3D ( 'NONE', #4627, #5253, #7736 ) ;
#856=AXIS2_PLACEMENT_3D ( 'NONE', #1926, #6841, #3852 ) ;
#868=LINE ( 'NONE', #1906, #6090 ) ;
#879=CIRCLE ( 'NONE', #356, 0.2149999999999995803 ) ;
#895=ORIENTED_EDGE ( 'NONE', *, *, #598, .T. ) ;
#898=VERTEX_POINT ( 'NONE', #406 ) ;
#901=ORIENTED_EDGE ( 'NONE', *, *, #2135, .F. ) ;
#902=ORIENTED_EDGE ( 'NONE', *, *, #3846, .T. ) ;
#903=DIRECTION ( 'NONE',  ( 0.7498009116086189474, -0.6531728565937869879, 0.1056589435873569599 ) ) ;
#915=DIRECTION ( 'NONE',  ( -0.000000000000000000, -0.000000000000000000, 1.000000000000000000 ) ) ;
#916=CARTESIAN_POINT ( 'NONE',  ( 6.185915932927993133, 0.4597367884986685582, 0.000000000000000000 ) ) ;
#926=ORIENTED_EDGE ( 'NONE', *, *, #6693, .T. ) ;
#934=FACE_OUTER_BOUND ( 'NONE', #142, .T. ) ;
#935=ORIENTED_EDGE ( 'NONE', *, *, #4194, .T. ) ;
#938=DIRECTION ( 'NONE',  ( -0.7540216022612858948, 0.6568496200222110337, 0.000000000000000000 ) ) ;
#947=DIRECTION ( 'NONE',  ( -0.000000000000000000, -0.000000000000000000, 1.000000000000000000 ) ) ;
#960=EDGE_LOOP ( 'NONE', ( #6283, #7111, #597, #7336 ) ) ;
#961=VECTOR ( 'NONE', #5920, 39.37007874015748143 ) ;
#963=VERTEX_POINT ( 'NONE', #6808 ) ;
#974=DIRECTION ( 'NONE',  ( -0.000000000000000000, 0.000000000000000000, 1.000000000000000000 ) ) ;
#976=CARTESIAN_POINT ( 'NONE',  ( -1.052129263295328521, 0.6378420796487936917, -0.09374999999999998612 ) ) ;
#977=CARTESIAN_POINT ( 'NONE',  ( 4.390472339057043705, -2.510390028880330249, -0.09374999999999998612 ) ) ;
#981=AXIS2_PLACEMENT_3D ( 'NONE', #1164, #7442, #6860 ) ;
#983=CARTESIAN_POINT ( 'NONE',  ( 3.672767723898985537, -8.314396374632453401, -0.1250000000000000000 ) ) ;
#988=ORIENTED_EDGE ( 'NONE', *, *, #2235, .F. ) ;
#989=EDGE_CURVE ( 'NONE', #2155, #7764, #3001, .T. ) ;
#993=EDGE_CURVE ( 'NONE', #2507, #5382, #1408, .T. ) ;
#1009=LINE ( 'NONE', #2309, #6101 ) ;
#1012=ORIENTED_EDGE ( 'NONE', *, *, #5031, .F. ) ;
#1013=AXIS2_PLACEMENT_3D ( 'NONE', #7554, #2377, #4358 ) ;
#1017=DIRECTION ( 'NONE',  ( 0.6568496200222107007, 0.7540216022612863389, -0.000000000000000000 ) ) ;
#1019=ORIENTED_EDGE ( 'NONE', *, *, #5646, .F. ) ;
#1020=LINE ( 'NONE', #6630, #814 ) ;
#1025=DIRECTION ( 'NONE',  ( 1.000000000000000000, 0.000000000000000000, 0.000000000000000000 ) ) ;
#1026=LINE ( 'NONE', #1101, #5715 ) ;
#1039=EDGE_CURVE ( 'NONE', #1869, #4782, #3698, .T. ) ;
#1043=LINE ( 'NONE', #6083, #6213 ) ;
#1049=DIRECTION ( 'NONE',  ( 1.000000000000000000, 0.000000000000000000, 0.000000000000000000 ) ) ;
#1050=DIRECTION ( 'NONE',  ( 0.04906492035527430795, -0.9987955914953422498, 0.000000000000000000 ) ) ;
#1058=CARTESIAN_POINT ( 'NONE',  ( -1.543211452806561690, 0.6927940070358462599, 0.1250000000000000000 ) ) ;
#1072=AXIS2_PLACEMENT_3D ( 'NONE', #269, #6421, #5325 ) ;
#1078=EDGE_CURVE ( 'NONE', #91, #6877, #4351, .T. ) ;
#1080=EDGE_CURVE ( 'NONE', #898, #3734, #5417, .T. ) ;
#1082=ORIENTED_EDGE ( 'NONE', *, *, #4949, .T. ) ;
#1085=EDGE_CURVE ( 'NONE', #2424, #5238, #4189, .T. ) ;
#1086=VERTEX_POINT ( 'NONE', #7581 ) ;
#1088=DIRECTION ( 'NONE',  ( 0.000000000000000000, -0.000000000000000000, -1.000000000000000000 ) ) ;
#1090=DIRECTION ( 'NONE',  ( 0.000000000000000000, 0.000000000000000000, 1.000000000000000000 ) ) ;
#1092=CARTESIAN_POINT ( 'NONE',  ( 3.659299226295303686, -8.245510427152350275, 5.393636709996481038 ) ) ;
#1098=DIRECTION ( 'NONE',  ( -0.7540216022612864499, 0.6568496200222104786, 0.000000000000000000 ) ) ;
#1101=CARTESIAN_POINT ( 'NONE',  ( -1.983451234524918227, 1.341543513548240529, -0.2959999999999997078 ) ) ;
#1102=EDGE_LOOP ( 'NONE', ( #6425, #1747, #4521, #7627, #6887, #1550 ) ) ;
#1103=ORIENTED_EDGE ( 'NONE', *, *, #6156, .T. ) ;
#1104=DIRECTION ( 'NONE',  ( -0.8680936205257663296, 0.4964005096718443477, -0.000000000000000000 ) ) ;
#1106=CIRCLE ( 'NONE', #981, 8.633908398497672110 ) ;
#1111=CARTESIAN_POINT ( 'NONE',  ( -0.9280291358773672394, 0.8548654847802351631, 0.09374999999999998612 ) ) ;
#1115=APPLICATION_CONTEXT ( 'configuration controlled 3d designs of mechanical parts and assemblies' ) ;
#1126=EDGE_CURVE ( 'NONE', #1869, #796, #7148, .T. ) ;
#1129=AXIS2_PLACEMENT_3D ( 'NONE', #4218, #7455, #6717 ) ;
#1131=DIRECTION ( 'NONE',  ( 1.000000000000000000, 1.049151427428407716E-10, 0.000000000000000000 ) ) ;
#1136=CIRCLE ( 'NONE', #742, 0.2499962251234248700 ) ;
#1140=CARTESIAN_POINT ( 'NONE',  ( -1.855136387357835481, 0.9645206712600612464, -0.08100000000000007194 ) ) ;
#1146=ORIENTED_EDGE ( 'NONE', *, *, #411, .F. ) ;
#1147=CIRCLE ( 'NONE', #7429, 0.2500000000000000555 ) ;
#1157=DIRECTION ( 'NONE',  ( -0.8680936205257663296, 0.4964005096718443477, 0.000000000000000000 ) ) ;
#1162=DIRECTION ( 'NONE',  ( 0.000000000000000000, -0.000000000000000000, -1.000000000000000000 ) ) ;
#1164=CARTESIAN_POINT ( 'NONE',  ( 3.672767464462126430, -8.314346814944791220, -0.1849999999999999978 ) ) ;
#1173=EDGE_LOOP ( 'NONE', ( #7603, #7692, #7516, #3259 ) ) ;
#1176=DIRECTION ( 'NONE',  ( -0.000000000000000000, 0.000000000000000000, -1.000000000000000000 ) ) ;
#1178=ADVANCED_FACE ( 'NONE', ( #1270 ), #4469, .T. ) ;
#1181=ADVANCED_FACE ( 'NONE', ( #620 ), #5776, .F. ) ;
#1183=DIRECTION ( 'NONE',  ( 0.000000000000000000, 0.000000000000000000, 1.000000000000000000 ) ) ;
#1188=FACE_OUTER_BOUND ( 'NONE', #2753, .T. ) ;
#1190=ORIENTED_EDGE ( 'NONE', *, *, #1680, .F. ) ;
#1192=CARTESIAN_POINT ( 'NONE',  ( 1.475891671935536831, 0.7226544316391477762, -0.1120558261758407559 ) ) ;
#1193=ORIENTED_EDGE ( 'NONE', *, *, #3385, .T. ) ;
#1199=AXIS2_PLACEMENT_3D ( 'NONE', #3254, #5795, #1360 ) ;
#1206=CYLINDRICAL_SURFACE ( 'NONE', #5337, 0.2499400561648078278 ) ;
#1209=ORIENTED_EDGE ( 'NONE', *, *, #7496, .F. ) ;
#1220=CARTESIAN_POINT ( 'NONE',  ( 6.068104892000602213, -0.009251957739379222667, 0.1849999999999999978 ) ) ;
#1230=DIRECTION ( 'NONE',  ( 0.000000000000000000, 0.000000000000000000, -1.000000000000000000 ) ) ;
#1234=CIRCLE ( 'NONE', #1352, 0.03124999999999999306 ) ;
#1235=EDGE_CURVE ( 'NONE', #340, #3734, #7053, .T. ) ;
#1237=ORIENTED_EDGE ( 'NONE', *, *, #6506, .F. ) ;
#1239=LINE ( 'NONE', #503, #6367 ) ;
#1256=CIRCLE ( 'NONE', #5848, 9.004497838701050583 ) ;
#1261=VECTOR ( 'NONE', #6819, 39.37007874015748143 ) ;
#1262=ORIENTED_EDGE ( 'NONE', *, *, #6829, .F. ) ;
#1267=CARTESIAN_POINT ( 'NONE',  ( -1.763177565995708296, 1.070083551578370207, -0.08100000000000007194 ) ) ;
#1268=AXIS2_PLACEMENT_3D ( 'NONE', #1946, #4454, #6949 ) ;
#1270=FACE_OUTER_BOUND ( 'NONE', #754, .T. ) ;
#1272=CARTESIAN_POINT ( 'NONE',  ( -3.165020334763531729, -1.163753072338894023, 0.1250000000000000000 ) ) ;
#1284=EDGE_CURVE ( 'NONE', #4126, #4355, #5586, .T. ) ;
#1288=CARTESIAN_POINT ( 'NONE',  ( -1.432604426929670494, 0.8194101287839825609, 0.1250000000000000000 ) ) ;
#1289=EDGE_CURVE ( 'NONE', #2344, #813, #364, .T. ) ;
#1293=LINE ( 'NONE', #3802, #5861 ) ;
#1294=LINE ( 'NONE', #1788, #5566 ) ;
#1297=CARTESIAN_POINT ( 'NONE',  ( -0.3566525292043903339, -0.3408511508279103985, 0.1250000000000000000 ) ) ;
#1298=DIRECTION ( 'NONE',  ( -0.9987955914953423608, -0.04906492035527378059, 0.000000000000000000 ) ) ;
#1302=ORIENTED_EDGE ( 'NONE', *, *, #378, .F. ) ;
#1310=CARTESIAN_POINT ( 'NONE',  ( 5.983714301115758083, -0.05774751952986264397, -0.1849999999999999978 ) ) ;
#1311=EDGE_CURVE ( 'NONE', #7782, #4068, #1631, .T. ) ;
#1315=ORIENTED_EDGE ( 'NONE', *, *, #2586, .F. ) ;
#1316=EDGE_CURVE ( 'NONE', #5686, #375, #5943, .T. ) ;
#1317=ORIENTED_EDGE ( 'NONE', *, *, #1284, .F. ) ;
#1318=CARTESIAN_POINT ( 'NONE',  ( 3.659299226295303686, -8.245510427152350275, 0.1850000000000003586 ) ) ;
#1319=EDGE_CURVE ( 'NONE', #358, #2750, #4029, .T. ) ;
#1321=PLANE ( 'NONE',  #7638 ) ;
#1324=CARTESIAN_POINT ( 'NONE',  ( 6.000000000000001776, 0.000000000000000000, 0.1250000000000004441 ) ) ;
#1325=ADVANCED_FACE ( 'NONE', ( #2700 ), #6531, .F. ) ;
#1332=ORIENTED_EDGE ( 'NONE', *, *, #6094, .T. ) ;
#1333=VECTOR ( 'NONE', #4909, 39.37007874015748143 ) ;
#1336=DIRECTION ( 'NONE',  ( 1.000000000000000000, 0.000000000000000000, 0.000000000000000000 ) ) ;
#1338=CIRCLE ( 'NONE', #5667, 8.633956053943499853 ) ;
#1343=AXIS2_PLACEMENT_3D ( 'NONE', #7003, #5151, #3923 ) ;
#1350=CARTESIAN_POINT ( 'NONE',  ( -1.432604426929670938, 0.8194101287839820058, -0.1250000000000000000 ) ) ;
#1352=AXIS2_PLACEMENT_3D ( 'NONE', #7811, #2239, #1050 ) ;
#1360=DIRECTION ( 'NONE',  ( 1.000000000000000000, 0.000000000000000000, 0.000000000000000000 ) ) ;
#1362=DIRECTION ( 'NONE',  ( 1.000000000000000000, 0.000000000000000000, -0.000000000000000000 ) ) ;
#1365=CIRCLE ( 'NONE', #2818, 8.696493751522730520 ) ;
#1366=EDGE_CURVE ( 'NONE', #6616, #6811, #5980, .T. ) ;
#1372=CARTESIAN_POINT ( 'NONE',  ( -2.114821033088378321, 1.190739337094255168, -0.2959999999999997078 ) ) ;
#1379=AXIS2_PLACEMENT_3D ( 'NONE', #1672, #2897, #3479 ) ;
#1385=ORIENTED_EDGE ( 'NONE', *, *, #3138, .T. ) ;
#1387=ORIENTED_EDGE ( 'NONE', *, *, #1039, .F. ) ;
#1389=CARTESIAN_POINT ( 'NONE',  ( 3.672767723898985537, -8.314396374632453401, 0.1250000000000000000 ) ) ;
#1391=ORIENTED_EDGE ( 'NONE', *, *, #6543, .F. ) ;
#1398=DIRECTION ( 'NONE',  ( -0.9987955914953423608, -0.04906492035527430795, -0.000000000000000000 ) ) ;
#1401=ORIENTED_EDGE ( 'NONE', *, *, #1289, .F. ) ;
#1407=ORIENTED_EDGE ( 'NONE', *, *, #3887, .F. ) ;
#1408=( BOUNDED_CURVE ( )  B_SPLINE_CURVE ( 3, ( #454, #5500, #1192, #5536 ),
 .UNSPECIFIED., .F., .T. ) 
 B_SPLINE_CURVE_WITH_KNOTS ( ( 4, 4 ),
 ( 1.570796326794900555, 3.141592653589790896 ),
 .UNSPECIFIED. ) 
 CURVE ( )  GEOMETRIC_REPRESENTATION_ITEM ( )  RATIONAL_B_SPLINE_CURVE ( ( 1.000000000000000000, 0.8047378541243663808, 0.8047378541243663808, 1.000000000000000000 ) ) 
 REPRESENTATION_ITEM ( '' )  );
#1409=ORIENTED_EDGE ( 'NONE', *, *, #1835, .T. ) ;
#1413=CARTESIAN_POINT ( 'NONE',  ( -1.067641779222573639, 0.6107141540073631747, -0.1250000000000000000 ) ) ;
#1414=ORIENTED_EDGE ( 'NONE', *, *, #8090, .T. ) ;
#1415=DIRECTION ( 'NONE',  ( 0.7540216022612858948, -0.6568496200222110337, 0.000000000000000000 ) ) ;
#1417=ADVANCED_FACE ( 'NONE', ( #6024 ), #4144, .T. ) ;
#1418=LINE ( 'NONE', #3472, #6836 ) ;
#1441=ORIENTED_EDGE ( 'NONE', *, *, #7537, .F. ) ;
#1442=CARTESIAN_POINT ( 'NONE',  ( -3.165020334763531729, -1.163753072338894023, 0.1250000000000000000 ) ) ;
#1448=VERTEX_POINT ( 'NONE', #7413 ) ;
#1455=CARTESIAN_POINT ( 'NONE',  ( 3.221700243049672174, 0.8684880333666047392, -0.1849999999999999978 ) ) ;
#1457=CARTESIAN_POINT ( 'NONE',  ( -1.855136387357835481, 0.9645206712600612464, 0.1339999999999995361 ) ) ;
#1469=CARTESIAN_POINT ( 'NONE',  ( 1.258616367985684104, -0.02482036785324303815, -0.1250000000000000000 ) ) ;
#1472=EDGE_CURVE ( 'NONE', #3734, #5716, #3875, .T. ) ;
#1479=EDGE_CURVE ( 'NONE', #789, #4769, #7158, .T. ) ;
#1480=CARTESIAN_POINT ( 'NONE',  ( 1.258671604940865274, -0.02501003737716508274, 5.393636709996481038 ) ) ;
#1481=EDGE_CURVE ( 'NONE', #3319, #2575, #1026, .T. ) ;
#1485=CIRCLE ( 'NONE', #6215, 8.573908398499121120 ) ;
#1487=CARTESIAN_POINT ( 'NONE',  ( 3.672798492683009286, -8.252032378159654513, 0.1850000000000003586 ) ) ;
#1488=VECTOR ( 'NONE', #6021, 39.37007874015748143 ) ;
#1491=DIRECTION ( 'NONE',  ( 0.6568496200222107007, 0.7540216022612862279, -0.000000000000000000 ) ) ;
#1498=ORIENTED_EDGE ( 'NONE', *, *, #1481, .F. ) ;
#1499=ORIENTED_EDGE ( 'NONE', *, *, #6903, .F. ) ;
#1503=CARTESIAN_POINT ( 'NONE',  ( -1.763177565995707630, 1.070083551578369763, -0.08100000000000007194 ) ) ;
#1507=DIRECTION ( 'NONE',  ( -0.000000000000000000, -0.000000000000000000, 1.000000000000000000 ) ) ;
#1508=AXIS2_PLACEMENT_3D ( 'NONE', #1977, #4568, #5725 ) ;
#1515=VECTOR ( 'NONE', #5115, 39.37007874015748143 ) ;
#1516=ORIENTED_EDGE ( 'NONE', *, *, #1879, .F. ) ;
#1523=ORIENTED_EDGE ( 'NONE', *, *, #7550, .T. ) ;
#1525=AXIS2_PLACEMENT_3D ( 'NONE', #6813, #3742, #4316 ) ;
#1530=ORIENTED_EDGE ( 'NONE', *, *, #7928, .F. ) ;
#1537=EDGE_CURVE ( 'NONE', #1539, #761, #30, .T. ) ;
#1539=VERTEX_POINT ( 'NONE', #3114 ) ;
#1541=APPLICATION_CONTEXT ( 'configuration controlled 3d designs of mechanical parts and assemblies' ) ;
#1546=EDGE_CURVE ( 'NONE', #4226, #7842, #7326, .T. ) ;
#1547=ORIENTED_EDGE ( 'NONE', *, *, #1690, .F. ) ;
#1550=ORIENTED_EDGE ( 'NONE', *, *, #170, .F. ) ;
#1552=CYLINDRICAL_SURFACE ( 'NONE', #3234, 0.03124999999999985428 ) ;
#1553=FACE_OUTER_BOUND ( 'NONE', #960, .T. ) ;
#1557=CARTESIAN_POINT ( 'NONE',  ( 3.659299226295303686, -8.245510427152350275, 5.393636709996481038 ) ) ;
#1572=LINE ( 'NONE', #5881, #224 ) ;
#1577=EDGE_CURVE ( 'NONE', #4309, #5382, #5768, .T. ) ;
#1586=EDGE_CURVE ( 'NONE', #6271, #5004, #1987, .T. ) ;
#1592=DIRECTION ( 'NONE',  ( -0.000000000000000000, -0.000000000000000000, -1.000000000000000000 ) ) ;
#1594=AXIS2_PLACEMENT_3D ( 'NONE', #1318, #4481, #672 ) ;
#1596=LINE ( 'NONE', #6118, #720 ) ;
#1600=ORIENTED_EDGE ( 'NONE', *, *, #1472, .T. ) ;
#1604=CARTESIAN_POINT ( 'NONE',  ( 6.213241126991890795, 0.5142750483228147873, 5.393636709996481038 ) ) ;
#1605=EDGE_LOOP ( 'NONE', ( #7908, #6833, #2955, #7046 ) ) ;
#1606=AXIS2_PLACEMENT_3D ( 'NONE', #7055, #662, #3162 ) ;
#1607=VERTEX_POINT ( 'NONE', #1837 ) ;
#1614=VERTEX_POINT ( 'NONE', #3845 ) ;
#1616=ORIENTED_EDGE ( 'NONE', *, *, #5131, .T. ) ;
#1617=ORIENTED_EDGE ( 'NONE', *, *, #6005, .T. ) ;
#1621=VERTEX_POINT ( 'NONE', #1955 ) ;
#1629=ADVANCED_FACE ( 'NONE', ( #1992 ), #4498, .T. ) ;
#1631=LINE ( 'NONE', #916, #2434 ) ;
#1633=CARTESIAN_POINT ( 'NONE',  ( -2.022862211726251136, 1.296302217412564017, -0.2959999999999997078 ) ) ;
#1638=CARTESIAN_POINT ( 'NONE',  ( 3.566133519791359507, 0.3212125039962153705, 0.000000000000000000 ) ) ;
#1644=AXIS2_PLACEMENT_3D ( 'NONE', #7216, #7715, #5955 ) ;
#1649=VERTEX_POINT ( 'NONE', #3308 ) ;
#1650=CARTESIAN_POINT ( 'NONE',  ( -1.052129263295328521, 0.6378420796487936917, 0.09374999999999998612 ) ) ;
#1653=AXIS2_PLACEMENT_3D ( 'NONE', #284, #2214, #4710 ) ;
#1654=AXIS2_PLACEMENT_3D ( 'NONE', #1503, #2115, #2768 ) ;
#1656=LINE ( 'NONE', #7274, #1754 ) ;
#1657=AXIS2_PLACEMENT_3D ( 'NONE', #1267, #2456, #1930 ) ;
#1658=FACE_OUTER_BOUND ( 'NONE', #3878, .T. ) ;
#1666=AXIS2_PLACEMENT_3D ( 'NONE', #2253, #4759, #2905 ) ;
#1672=CARTESIAN_POINT ( 'NONE',  ( -0.9280291358773672394, 0.8548654847802351631, -0.09374999999999998612 ) ) ;
#1675=ORIENTED_EDGE ( 'NONE', *, *, #3188, .T. ) ;
#1677=( BOUNDED_CURVE ( )  B_SPLINE_CURVE ( 3, ( #6560, #2212, #7934, #3438 ),
 .UNSPECIFIED., .F., .T. ) 
 B_SPLINE_CURVE_WITH_KNOTS ( ( 4, 4 ),
 ( 2.185478394931412941E-15, 1.570796326794896558 ),
 .UNSPECIFIED. ) 
 CURVE ( )  GEOMETRIC_REPRESENTATION_ITEM ( )  RATIONAL_B_SPLINE_CURVE ( ( 1.000000000000000000, 0.8047378541243654926, 0.8047378541243654926, 1.000000000000000000 ) ) 
 REPRESENTATION_ITEM ( '' )  );
#1678=ADVANCED_FACE ( 'NONE', ( #189 ), #5201, .T. ) ;
#1680=EDGE_CURVE ( 'NONE', #4572, #6392, #1418, .T. ) ;
#1685=ADVANCED_FACE ( 'NONE', ( #1553 ), #7700, .F. ) ;
#1687=DIRECTION ( 'NONE',  ( -0.000000000000000000, -0.000000000000000000, 1.000000000000000000 ) ) ;
#1690=EDGE_CURVE ( 'NONE', #4981, #358, #7076, .T. ) ;
#1693=ORIENTED_EDGE ( 'NONE', *, *, #6397, .T. ) ;
#1697=CARTESIAN_POINT ( 'NONE',  ( 1.258671604940864608, -0.02501003737716508274, 5.393636709996481038 ) ) ;
#1707=DIRECTION ( 'NONE',  ( -0.6568496200222107007, -0.7540216022612863389, 0.000000000000000000 ) ) ;
#1712=ORIENTED_EDGE ( 'NONE', *, *, #989, .T. ) ;
#1715=DIRECTION ( 'NONE',  ( 1.000000000000000000, 0.000000000000000000, 0.000000000000000000 ) ) ;
#1716=DIRECTION ( 'NONE',  ( -1.000000000000000000, 0.000000000000000000, 0.000000000000000000 ) ) ;
#1718=ORIENTED_EDGE ( 'NONE', *, *, #3260, .T. ) ;
#1719=DIRECTION ( 'NONE',  ( -0.000000000000000000, 0.000000000000000000, 1.000000000000000000 ) ) ;
#1720=( BOUNDED_CURVE ( )  B_SPLINE_CURVE ( 3, ( #748, #2060, #5781, #1350 ),
 .UNSPECIFIED., .F., .T. ) 
 B_SPLINE_CURVE_WITH_KNOTS ( ( 4, 4 ),
 ( 3.141592653589793116, 4.712388980384674575 ),
 .UNSPECIFIED. ) 
 CURVE ( )  GEOMETRIC_REPRESENTATION_ITEM ( )  RATIONAL_B_SPLINE_CURVE ( ( 1.000000000000000000, 0.8047378541243684902, 0.8047378541243684902, 1.000000000000000000 ) ) 
 REPRESENTATION_ITEM ( '' )  );
#1722=PLANE ( 'NONE',  #1994 ) ;
#1723=EDGE_CURVE ( 'NONE', #358, #4885, #5242, .T. ) ;
#1725=ADVANCED_FACE ( 'NONE', ( #7122 ), #3431, .T. ) ;
#1729=AXIS2_PLACEMENT_3D ( 'NONE', #6310, #767, #1336 ) ;
#1731=EDGE_CURVE ( 'NONE', #845, #6740, #4546, .T. ) ;
#1736=DIRECTION ( 'NONE',  ( -0.000000000000000000, -0.000000000000000000, 1.000000000000000000 ) ) ;
#1738=ORIENTED_EDGE ( 'NONE', *, *, #7090, .F. ) ;
#1742=AXIS2_PLACEMENT_3D ( 'NONE', #6564, #3976, #5257 ) ;
#1746=CARTESIAN_POINT ( 'NONE',  ( -1.723766588794375387, 1.115324847714046497, 0.1339999999999995361 ) ) ;
#1747=ORIENTED_EDGE ( 'NONE', *, *, #1723, .T. ) ;
#1750=ORIENTED_EDGE ( 'NONE', *, *, #1723, .F. ) ;
#1753=CIRCLE ( 'NONE', #2665, 9.064497838702109789 ) ;
#1754=VECTOR ( 'NONE', #903, 39.37007874015748143 ) ;
#1767=VECTOR ( 'NONE', #5620, 39.37007874015748143 ) ;
#1768=ORIENTED_EDGE ( 'NONE', *, *, #6204, .F. ) ;
#1780=FACE_OUTER_BOUND ( 'NONE', #8091, .T. ) ;
#1781=VECTOR ( 'NONE', #7133, 39.37007874015748143 ) ;
#1783=ADVANCED_FACE ( 'NONE', ( #2207 ), #7203, .T. ) ;
#1787=CARTESIAN_POINT ( 'NONE',  ( 6.317381622560545473, 0.2407432673787524013, -0.1849999999999999978 ) ) ;
#1788=CARTESIAN_POINT ( 'NONE',  ( 1.475891671935536609, 0.7226544316391472211, 0.1849999999999999978 ) ) ;
#1793=DIRECTION ( 'NONE',  ( 0.7540216022612863389, -0.6568496200222107007, 0.000000000000000000 ) ) ;
#1796=CIRCLE ( 'NONE', #6374, 8.573908398499121120 ) ;
#1803=VECTOR ( 'NONE', #7599, 39.37007874015748143 ) ;
#1813=DIRECTION ( 'NONE',  ( -0.000000000000000000, 0.000000000000000000, 1.000000000000000000 ) ) ;
#1815=CARTESIAN_POINT ( 'NONE',  ( -0.9280291358773672394, 0.8548654847802351631, 0.09374999999999998612 ) ) ;
#1819=ADVANCED_FACE ( 'NONE', ( #7241 ), #7883, .F. ) ;
#1823=EDGE_LOOP ( 'NONE', ( #6295, #3276, #1407, #3297 ) ) ;
#1826=CARTESIAN_POINT ( 'NONE',  ( 3.672798492683009286, -8.252032378159654513, 0.1850000000000003586 ) ) ;
#1828=CARTESIAN_POINT ( 'NONE',  ( -0.9142296270274463676, 0.5739542246721701657, -0.09374999999999998612 ) ) ;
#1834=DIRECTION ( 'NONE',  ( 0.000000000000000000, 0.000000000000000000, -1.000000000000000000 ) ) ;
#1835=EDGE_CURVE ( 'NONE', #3658, #6616, #1020, .T. ) ;
#1836=EDGE_CURVE ( 'NONE', #340, #1448, #8003, .T. ) ;
#1837=CARTESIAN_POINT ( 'NONE',  ( 1.356840083662244956, 0.003162463486408387866, 0.1250000000000000278 ) ) ;
#1838=ORIENTED_EDGE ( 'NONE', *, *, #1085, .T. ) ;
#1850=CARTESIAN_POINT ( 'NONE',  ( 3.672798492683009286, -8.252032378159654513, 0.1250000000000004441 ) ) ;
#1853=LINE ( 'NONE', #632, #596 ) ;
#1858=DIRECTION ( 'NONE',  ( -0.000000000000000000, -0.000000000000000000, 1.000000000000000000 ) ) ;
#1863=CARTESIAN_POINT ( 'NONE',  ( -1.543211452806561690, 0.6927940070358462599, -0.1250000000000000000 ) ) ;
#1868=VECTOR ( 'NONE', #202, 39.37007874015748143 ) ;
#1869=VERTEX_POINT ( 'NONE', #2241 ) ;
#1878=CYLINDRICAL_SURFACE ( 'NONE', #1343, 8.573908398499121120 ) ;
#1879=EDGE_CURVE ( 'NONE', #1614, #7167, #6189, .T. ) ;
#1883=ORIENTED_EDGE ( 'NONE', *, *, #6393, .T. ) ;
#1888=EDGE_LOOP ( 'NONE', ( #6030, #379, #387, #7947, #6151, #7268, #5762, #6134 ) ) ;
#1891=ORIENTED_EDGE ( 'NONE', *, *, #2363, .T. ) ;
#1892=CARTESIAN_POINT ( 'NONE',  ( 4.405984854984288823, -2.483262103238899954, 0.1250000000000000000 ) ) ;
#1898=DIRECTION ( 'NONE',  ( 1.000000000000000000, 0.000000000000000000, 0.000000000000000000 ) ) ;
#1899=CIRCLE ( 'NONE', #855, 0.1249999999999998473 ) ;
#1906=CARTESIAN_POINT ( 'NONE',  ( 5.983714301115758083, -0.05774751952986264397, 5.393636709996481038 ) ) ;
#1912=AXIS2_PLACEMENT_3D ( 'NONE', #2720, #5231, #5428 ) ;
#1915=ORIENTED_EDGE ( 'NONE', *, *, #2015, .F. ) ;
#1918=CARTESIAN_POINT ( 'NONE',  ( 1.258616368121236118, -0.02482036781376564805, -0.1250000000000000000 ) ) ;
#1922=FACE_BOUND ( 'NONE', #3834, .T. ) ;
#1923=CIRCLE ( 'NONE', #7288, 9.064497838702109789 ) ;
#1926=CARTESIAN_POINT ( 'NONE',  ( 3.666415866878781848, -8.185094079965441694, -0.1849999999999999978 ) ) ;
#1930=DIRECTION ( 'NONE',  ( -0.7540216022612861169, 0.6568496200222108117, 0.000000000000000000 ) ) ;
#1932=VECTOR ( 'NONE', #7304, 39.37007874015748143 ) ;
#1933=ORIENTED_EDGE ( 'NONE', *, *, #4747, .T. ) ;
#1937=DIRECTION ( 'NONE',  ( -0.4964005096718412946, -0.8680936205257682170, 0.000000000000000000 ) ) ;
#1940=DIRECTION ( 'NONE',  ( -0.4964005096718455134, -0.8680936205257656635, 0.000000000000000000 ) ) ;
#1946=CARTESIAN_POINT ( 'NONE',  ( 3.666415866878782737, -8.185094079965432812, 0.1849999999999999978 ) ) ;
#1951=CARTESIAN_POINT ( 'NONE',  ( 3.666415866878781848, -8.185094079965441694, -0.1849999999999999978 ) ) ;
#1955=CARTESIAN_POINT ( 'NONE',  ( -1.803041671366328202, 1.104810305277057259, -0.3269762307749163877 ) ) ;
#1959=CARTESIAN_POINT ( 'NONE',  ( 0.000000000000000000, 0.000000000000000000, 0.1250000000000000000 ) ) ;
#1964=LINE ( 'NONE', #5665, #1868 ) ;
#1970=ORIENTED_EDGE ( 'NONE', *, *, #7974, .T. ) ;
#1971=ADVANCED_FACE ( 'NONE', ( #2442 ), #7716, .T. ) ;
#1975=SHAPE_DEFINITION_REPRESENTATION ( #5984, #2 ) ;
#1977=CARTESIAN_POINT ( 'NONE',  ( 3.659299226295303686, -8.245510427152350275, -0.1849999999999999978 ) ) ;
#1978=EDGE_CURVE ( 'NONE', #813, #5374, #3966, .T. ) ;
#1987=CIRCLE ( 'NONE', #1729, 0.4999999999999997224 ) ;
#1989=CARTESIAN_POINT ( 'NONE',  ( 6.190221022838899856, 0.4584861219976859026, -0.1849999999999999978 ) ) ;
#1992=FACE_OUTER_BOUND ( 'NONE', #6458, .T. ) ;
#1994=AXIS2_PLACEMENT_3D ( 'NONE', #2342, #6125, #7340 ) ;
#2000=DIRECTION ( 'NONE',  ( -1.000000000000000000, 0.000000000000000000, 0.000000000000000000 ) ) ;
#2014=ORIENTED_EDGE ( 'NONE', *, *, #4346, .T. ) ;
#2015=EDGE_CURVE ( 'NONE', #5187, #6313, #5276, .T. ) ;
#2017=ORIENTED_EDGE ( 'NONE', *, *, #4054, .T. ) ;
#2023=CARTESIAN_POINT ( 'NONE',  ( 1.353816004522938599, 0.002313473902802895728, -0.1850000000000455724 ) ) ;
#2024=ORIENTED_EDGE ( 'NONE', *, *, #3533, .T. ) ;
#2026=EDGE_CURVE ( 'NONE', #2766, #2552, #6571, .T. ) ;
#2030=CYLINDRICAL_SURFACE ( 'NONE', #2277, 9.004497838701052359 ) ;
#2037=DIRECTION ( 'NONE',  ( 0.7540216022612864499, -0.6568496200222104786, 0.000000000000000000 ) ) ;
#2045=DIRECTION ( 'NONE',  ( 1.000000000000000000, 0.000000000000000000, 0.000000000000000000 ) ) ;
#2053=DIRECTION ( 'NONE',  ( -0.000000000000000000, -0.000000000000000000, 1.000000000000000000 ) ) ;
#2060=CARTESIAN_POINT ( 'NONE',  ( -1.411633252941551175, 0.8434166392007481639, -0.1120558261758405477 ) ) ;
#2066=DIRECTION ( 'NONE',  ( 0.7531131608245043019, -0.6578909993250587895, 0.000000000000000000 ) ) ;
#2068=LINE ( 'NONE', #7761, #2443 ) ;
#2078=CARTESIAN_POINT ( 'NONE',  ( 3.221700243049672174, 0.8684880333666047392, 0.1850000000000003586 ) ) ;
#2093=LINE ( 'NONE', #1469, #7763 ) ;
#2107=ORIENTED_EDGE ( 'NONE', *, *, #4346, .F. ) ;
#2108=ORIENTED_EDGE ( 'NONE', *, *, #5694, .F. ) ;
#2112=CARTESIAN_POINT ( 'NONE',  ( 6.000000000000001776, 0.000000000000000000, -0.1250000000000004441 ) ) ;
#2115=DIRECTION ( 'NONE',  ( 0.6568496200222108117, 0.7540216022612861169, 0.000000000000000000 ) ) ;
#2116=DIRECTION ( 'NONE',  ( 0.000000000000000000, 0.000000000000000000, -1.000000000000000000 ) ) ;
#2118=CYLINDRICAL_SURFACE ( 'NONE', #5811, 8.633908398497670333 ) ;
#2121=ADVANCED_FACE ( 'NONE', ( #4886, #2495, #7428 ), #1722, .F. ) ;
#2128=DIRECTION ( 'NONE',  ( -0.000000000000000000, 0.000000000000000000, -1.000000000000000000 ) ) ;
#2130=CIRCLE ( 'NONE', #5802, 0.4060000000000000830 ) ;
#2135=EDGE_CURVE ( 'NONE', #2575, #4907, #3036, .T. ) ;
#2142=CARTESIAN_POINT ( 'NONE',  ( 1.290272380711668720, -0.01560121663631008383, -0.1250000000000000278 ) ) ;
#2144=EDGE_CURVE ( 'NONE', #4981, #1649, #6729, .T. ) ;
#2155=VERTEX_POINT ( 'NONE', #3738 ) ;
#2157=AXIS2_PLACEMENT_3D ( 'NONE', #7997, #1858, #470 ) ;
#2159=ORIENTED_EDGE ( 'NONE', *, *, #5595, .T. ) ;
#2169=EDGE_LOOP ( 'NONE', ( #1600, #413, #2917, #769, #7266, #3171 ) ) ;
#2170=VECTOR ( 'NONE', #4319, 39.37007874015748143 ) ;
#2174=CARTESIAN_POINT ( 'NONE',  ( -1.411841654243101596, 0.8435981834898315102, 0.1250000000000000000 ) ) ;
#2185=CIRCLE ( 'NONE', #7807, 0.03124999999999996184 ) ;
#2189=ADVANCED_FACE ( 'NONE', ( #5463 ), #2371, .T. ) ;
#2192=ORIENTED_EDGE ( 'NONE', *, *, #1289, .T. ) ;
#2196=DIRECTION ( 'NONE',  ( -0.9987955914953420278, -0.04906492035527816598, 0.000000000000000000 ) ) ;
#2207=FACE_OUTER_BOUND ( 'NONE', #324, .T. ) ;
#2208=EDGE_LOOP ( 'NONE', ( #7830, #4073, #8069, #1883 ) ) ;
#2211=EDGE_LOOP ( 'NONE', ( #2159, #2024, #6229, #3940, #6245, #5675 ) ) ;
#2212=CARTESIAN_POINT ( 'NONE',  ( 1.475891671935536165, 0.7226544316391469991, 0.1120558261758407698 ) ) ;
#2213=LINE ( 'NONE', #1058, #6891 ) ;
#2214=DIRECTION ( 'NONE',  ( 0.000000000000000000, 0.000000000000000000, -1.000000000000000000 ) ) ;
#2231=DIRECTION ( 'NONE',  ( -0.000000000000000000, -0.000000000000000000, -1.000000000000000000 ) ) ;
#2235=EDGE_CURVE ( 'NONE', #1607, #6273, #4616, .T. ) ;
#2239=DIRECTION ( 'NONE',  ( -0.9987955914953422498, -0.04906492035527344059, 0.000000000000000000 ) ) ;
#2240=DIRECTION ( 'NONE',  ( 0.7540216022612862279, -0.6568496200222107007, 0.000000000000000000 ) ) ;
#2241=CARTESIAN_POINT ( 'NONE',  ( 6.185915932928153005, 0.4597367884986204856, -0.1849999999999999978 ) ) ;
#2247=EDGE_LOOP ( 'NONE', ( #6447, #7209, #228, #1718, #298, #1414, #6780, #7069, #6233 ) ) ;
#2253=CARTESIAN_POINT ( 'NONE',  ( 3.672798492683009286, -8.252032378159654513, 5.393636709996481038 ) ) ;
#2257=CARTESIAN_POINT ( 'NONE',  ( -1.803041671366328202, 1.104810305277057259, -0.3269762307749163877 ) ) ;
#2273=DIRECTION ( 'NONE',  ( -0.000000000000000000, -0.000000000000000000, -1.000000000000000000 ) ) ;
#2277=AXIS2_PLACEMENT_3D ( 'NONE', #1951, #6417, #3918 ) ;
#2284=DIRECTION ( 'NONE',  ( -1.000000000000000000, 0.000000000000000000, 0.000000000000000000 ) ) ;
#2287=EDGE_CURVE ( 'NONE', #1539, #5845, #3819, .T. ) ;
#2296=ORIENTED_EDGE ( 'NONE', *, *, #170, .T. ) ;
#2300=DIRECTION ( 'NONE',  ( 1.000000000000000000, 0.000000000000000000, 0.000000000000000000 ) ) ;
#2304=CIRCLE ( 'NONE', #6893, 8.573908398499121120 ) ;
#2306=CARTESIAN_POINT ( 'NONE',  ( -1.411633252941551619, 0.8434166392007494961, -0.09374999999999998612 ) ) ;
#2309=CARTESIAN_POINT ( 'NONE',  ( -0.3566525292043903339, -0.3408511508279103985, 0.1250000000000000000 ) ) ;
#2313=CARTESIAN_POINT ( 'NONE',  ( -3.165020334763531729, -1.163753072338894023, -0.1250000000000000000 ) ) ;
#2316=CARTESIAN_POINT ( 'NONE',  ( 3.672767723898985537, -8.314396374632453401, 0.1250000000000000000 ) ) ;
#2321=EDGE_CURVE ( 'NONE', #789, #6740, #1338, .T. ) ;
#2323=ORIENTED_EDGE ( 'NONE', *, *, #373, .T. ) ;
#2328=DIRECTION ( 'NONE',  ( 1.000000000000000000, 0.000000000000000000, 0.000000000000000000 ) ) ;
#2330=EDGE_CURVE ( 'NONE', #4907, #6616, #2130, .T. ) ;
#2332=ORIENTED_EDGE ( 'NONE', *, *, #5031, .T. ) ;
#2342=CARTESIAN_POINT ( 'NONE',  ( 3.690413561029368683, -8.374393170229348371, 0.1849999999999999978 ) ) ;
#2343=VERTEX_POINT ( 'NONE', #6970 ) ;
#2344=VERTEX_POINT ( 'NONE', #7618 ) ;
#2349=DIRECTION ( 'NONE',  ( -1.000000000000000000, 0.000000000000000000, 0.000000000000000000 ) ) ;
#2350=CARTESIAN_POINT ( 'NONE',  ( 6.067386035484807039, 0.2407470087491024868, 0.1849999999999999978 ) ) ;
#2363=EDGE_CURVE ( 'NONE', #6856, #365, #6712, .T. ) ;
#2365=CARTESIAN_POINT ( 'NONE',  ( 6.191327929239392347, 0.4578608198540764507, -0.1250000000000000000 ) ) ;
#2371=PLANE ( 'NONE',  #7366 ) ;
#2374=EDGE_CURVE ( 'NONE', #4226, #5921, #4439, .T. ) ;
#2377=DIRECTION ( 'NONE',  ( -0.000000000000000000, -0.000000000000000000, -1.000000000000000000 ) ) ;
#2382=LINE ( 'NONE', #1697, #2170 ) ;
#2385=ADVANCED_BREP_SHAPE_REPRESENTATION ( '', ( #6445, #6285, #3555 ), #5783 ) ;
#2386=ORIENTED_EDGE ( 'NONE', *, *, #1078, .T. ) ;
#2388=DIRECTION ( 'NONE',  ( 0.000000000000000000, 0.000000000000000000, 1.000000000000000000 ) ) ;
#2392=CARTESIAN_POINT ( 'NONE',  ( -1.555749437692314885, 0.7037162015503708457, -0.1657613293278376587 ) ) ;
#2396=DIRECTION ( 'NONE',  ( 0.9987955914953421388, 0.04906492035527377366, -0.000000000000000000 ) ) ;
#2398=EDGE_LOOP ( 'NONE', ( #7164, #4495, #1516, #4412 ) ) ;
#2400=DIRECTION ( 'NONE',  ( 0.6568496200222108117, 0.7540216022612861169, 0.000000000000000000 ) ) ;
#2403=CARTESIAN_POINT ( 'NONE',  ( 4.390472339057044593, -2.510390028880329805, 0.1250000000000000000 ) ) ;
#2406=CARTESIAN_POINT ( 'NONE',  ( -1.723766588794375387, 1.115324847714046497, -0.08100000000000007194 ) ) ;
#2410=CARTESIAN_POINT ( 'NONE',  ( -1.803041671366327314, 1.104810305277056592, 0.1649762307749162715 ) ) ;
#2413=AXIS2_PLACEMENT_3D ( 'NONE', #2406, #3029, #6802 ) ;
#2414=VERTEX_POINT ( 'NONE', #6932 ) ;
#2419=DIMENSIONAL_EXPONENTS ( 1.000000000000000000, 0.000000000000000000, 0.000000000000000000, 0.000000000000000000, 0.000000000000000000, 0.000000000000000000, 0.000000000000000000 ) ;
#2421=DIRECTION ( 'NONE',  ( 0.000000000000000000, 0.000000000000000000, -1.000000000000000000 ) ) ;
#2422=EDGE_CURVE ( 'NONE', #4959, #3419, #1964, .T. ) ;
#2423=EDGE_CURVE ( 'NONE', #5238, #5382, #3859, .T. ) ;
#2424=VERTEX_POINT ( 'NONE', #6359 ) ;
#2426=ADVANCED_FACE ( 'NONE', ( #4558 ), #2703, .F. ) ;
#2433=CARTESIAN_POINT ( 'NONE',  ( 6.185915932927993133, 0.4597367884986663933, 0.1850000000000003586 ) ) ;
#2434=VECTOR ( 'NONE', #947, 39.37007874015748143 ) ;
#2439=ORIENTED_EDGE ( 'NONE', *, *, #1731, .F. ) ;
#2440=VECTOR ( 'NONE', #6956, 39.37007874015748143 ) ;
#2442=FACE_OUTER_BOUND ( 'NONE', #385, .T. ) ;
#2443=VECTOR ( 'NONE', #7337, 39.37007874015748143 ) ;
#2445=CARTESIAN_POINT ( 'NONE',  ( 1.258616367985684104, -0.02482036785324303815, -0.1849999999999999978 ) ) ;
#2446=DIRECTION ( 'NONE',  ( 0.7540216022612857838, -0.6568496200222112558, 7.922359181626369842E-15 ) ) ;
#2447=ORIENTED_EDGE ( 'NONE', *, *, #22, .F. ) ;
#2450=VECTOR ( 'NONE', #5456, 39.37007874015748854 ) ;
#2456=DIRECTION ( 'NONE',  ( 0.6568496200222109227, 0.7540216022612862279, 0.000000000000000000 ) ) ;
#2459=ORIENTED_EDGE ( 'NONE', *, *, #2321, .F. ) ;
#2462=CYLINDRICAL_SURFACE ( 'NONE', #1013, 8.696493751522730520 ) ;
#2486=CARTESIAN_POINT ( 'NONE',  ( 6.213241126991893459, 0.5142750483228205605, 0.1850000000000003586 ) ) ;
#2494=ORIENTED_EDGE ( 'NONE', *, *, #6589, .F. ) ;
#2495=FACE_BOUND ( 'NONE', #6376, .T. ) ;
#2507=VERTEX_POINT ( 'NONE', #7210 ) ;
#2512=CARTESIAN_POINT ( 'NONE',  ( 1.258671604940865274, -0.02501003737716508274, 0.1850000000000003586 ) ) ;
#2513=CARTESIAN_POINT ( 'NONE',  ( 6.190221022838899856, 0.4584861219976859026, 0.1850000000000003586 ) ) ;
#2515=ORIENTED_EDGE ( 'NONE', *, *, #5131, .F. ) ;
#2520=DIRECTION ( 'NONE',  ( 0.7540216022612863389, -0.6568496200222107007, 0.000000000000000000 ) ) ;
#2521=EDGE_CURVE ( 'NONE', #3224, #4959, #7088, .T. ) ;
#2526=AXIS2_PLACEMENT_3D ( 'NONE', #1140, #3021, #1793 ) ;
#2527=CARTESIAN_POINT ( 'NONE',  ( 1.475891671935536609, 0.7226544316391472211, 0.1850000000000003586 ) ) ;
#2528=EDGE_CURVE ( 'NONE', #91, #7381, #5804, .T. ) ;
#2544=FACE_OUTER_BOUND ( 'NONE', #5367, .T. ) ;
#2552=VERTEX_POINT ( 'NONE', #2746 ) ;
#2554=LENGTH_MEASURE_WITH_UNIT ( LENGTH_MEASURE( 0.02539999999999999897 ), #3173 );
#2557=CARTESIAN_POINT ( 'NONE',  ( -1.723766588794375387, 1.115324847714046497, -0.2959999999999997078 ) ) ;
#2558=PLANE ( 'NONE',  #5697 ) ;
#2565=AXIS2_PLACEMENT_3D ( 'NONE', #195, #6389, #3854 ) ;
#2568=CARTESIAN_POINT ( 'NONE',  ( -1.432604426929670494, 0.8194101287839825609, 0.1250000000000000000 ) ) ;
#2572=ADVANCED_FACE ( 'NONE', ( #7135 ), #5411, .F. ) ;
#2575=VERTEX_POINT ( 'NONE', #1633 ) ;
#2576=CARTESIAN_POINT ( 'NONE',  ( -0.9142296270274463676, 0.5739542246721696106, 0.1250000000000000000 ) ) ;
#2583=CARTESIAN_POINT ( 'NONE',  ( 1.258616367985684104, -0.02482036785324303815, -0.1849999999999999978 ) ) ;
#2586=EDGE_CURVE ( 'NONE', #6313, #2507, #2093, .T. ) ;
#2595=DIRECTION ( 'NONE',  ( 1.000000000000000000, 0.000000000000000000, 0.000000000000000000 ) ) ;
#2596=ORIENTED_EDGE ( 'NONE', *, *, #1586, .T. ) ;
#2602=ORIENTED_EDGE ( 'NONE', *, *, #4851, .T. ) ;
#2620=ORIENTED_EDGE ( 'NONE', *, *, #7827, .T. ) ;
#2626=SHAPE_REPRESENTATION_RELATIONSHIP ( 'NONE' , 'NONE' ,  #2, #2385 ) ;
#2633=EDGE_LOOP ( 'NONE', ( #1547, #7969, #1391, #1750 ) ) ;
#2643=CARTESIAN_POINT ( 'NONE',  ( -1.723766588794375387, 1.115324847714046497, -0.08100000000000007194 ) ) ;
#2644=DIRECTION ( 'NONE',  ( -0.000000000000000000, 0.000000000000000000, 1.000000000000000000 ) ) ;
#2646=ORIENTED_EDGE ( 'NONE', *, *, #6845, .F. ) ;
#2647=EDGE_CURVE ( 'NONE', #158, #1448, #6188, .T. ) ;
#2659=EDGE_CURVE ( 'NONE', #4174, #4226, #7973, .T. ) ;
#2665=AXIS2_PLACEMENT_3D ( 'NONE', #4739, #7237, #4206 ) ;
#2670=ORIENTED_EDGE ( 'NONE', *, *, #6942, .F. ) ;
#2672=CARTESIAN_POINT ( 'NONE',  ( 1.475891671935536609, 0.7226544316391472211, -0.09375000000000005551 ) ) ;
#2676=ORIENTED_EDGE ( 'NONE', *, *, #1126, .T. ) ;
#2680=EDGE_CURVE ( 'NONE', #2343, #2766, #3445, .T. ) ;
#2682=DIRECTION ( 'NONE',  ( -0.07966912593697395018, 0.06940203694730379125, -0.9944024274105548455 ) ) ;
#2693=CIRCLE ( 'NONE', #1525, 0.2499400561648078278 ) ;
#2696=AXIS2_PLACEMENT_3D ( 'NONE', #6798, #7329, #2988 ) ;
#2699=FACE_OUTER_BOUND ( 'NONE', #4927, .T. ) ;
#2700=FACE_OUTER_BOUND ( 'NONE', #5036, .T. ) ;
#2702=AXIS2_PLACEMENT_3D ( 'NONE', #3468, #2240, #7880 ) ;
#2703=PLANE ( 'NONE',  #1606 ) ;
#2706=AXIS2_PLACEMENT_3D ( 'NONE', #615, #5532, #6724 ) ;
#2707=DIRECTION ( 'NONE',  ( -0.6568496200222107007, -0.7540216022612862279, 0.000000000000000000 ) ) ;
#2720=CARTESIAN_POINT ( 'NONE',  ( 3.690413561029368683, -8.374393170229348371, 0.1849999999999999978 ) ) ;
#2727=ORIENTED_EDGE ( 'NONE', *, *, #2647, .F. ) ;
#2744=CARTESIAN_POINT ( 'NONE',  ( -1.803041671366327314, 1.104810305277056592, 0.1649762307749162715 ) ) ;
#2746=CARTESIAN_POINT ( 'NONE',  ( 6.213241126991890795, 0.5142750483228147873, -0.1849999999999999978 ) ) ;
#2747=DIRECTION ( 'NONE',  ( 0.000000000000000000, 0.000000000000000000, -1.000000000000000000 ) ) ;
#2750=VERTEX_POINT ( 'NONE', #2527 ) ;
#2752=DIRECTION ( 'NONE',  ( 0.2815666759589948720, -0.9595416650617117904, 0.000000000000000000 ) ) ;
#2753=EDGE_LOOP ( 'NONE', ( #2296, #2853, #6918, #2439, #2811 ) ) ;
#2754=FACE_OUTER_BOUND ( 'NONE', #1102, .T. ) ;
#2761=PRODUCT ( 'Cleco, Handle, Stationary', 'Cleco, Handle, Stationary', '', ( #56 ) ) ;
#2763=ORIENTED_EDGE ( 'NONE', *, *, #1479, .F. ) ;
#2764=CARTESIAN_POINT ( 'NONE',  ( 1.275565605498405253, -0.08258253728086821510, 5.393636709996481038 ) ) ;
#2766=VERTEX_POINT ( 'NONE', #2486 ) ;
#2768=DIRECTION ( 'NONE',  ( -0.7540216022612858948, 0.6568496200222110337, 0.000000000000000000 ) ) ;
#2769=DIRECTION ( 'NONE',  ( -0.04906492035527430795, 0.9987955914953422498, 0.000000000000000000 ) ) ;
#2770=ORIENTED_EDGE ( 'NONE', *, *, #2528, .T. ) ;
#2776=EDGE_LOOP ( 'NONE', ( #7850, #4571 ) ) ;
#2790=ADVANCED_FACE ( 'NONE', ( #3773 ), #3192, .T. ) ;
#2795=CARTESIAN_POINT ( 'NONE',  ( -1.411633252941551619, 0.8434166392007494961, 0.1250000000000000000 ) ) ;
#2797=ORIENTED_EDGE ( 'NONE', *, *, #4786, .F. ) ;
#2800=EDGE_LOOP ( 'NONE', ( #4552, #4510, #5467, #537 ) ) ;
#2802=ORIENTED_EDGE ( 'NONE', *, *, #7496, .T. ) ;
#2811=ORIENTED_EDGE ( 'NONE', *, *, #2991, .F. ) ;
#2814=PLANE ( 'NONE',  #6870 ) ;
#2818=AXIS2_PLACEMENT_3D ( 'NONE', #4830, #2273, #6100 ) ;
#2822=AXIS2_PLACEMENT_3D ( 'NONE', #3090, #2421, #6779 ) ;
#2824=DIRECTION ( 'NONE',  ( -0.6568496200222107007, -0.7540216022612863389, 0.000000000000000000 ) ) ;
#2830=ADVANCED_FACE ( 'NONE', ( #3886, #1922 ), #3154, .T. ) ;
#2840=CARTESIAN_POINT ( 'NONE',  ( 1.353740795342265546, 0.002292344206094486941, -0.1250000000000000000 ) ) ;
#2845=ORIENTED_EDGE ( 'NONE', *, *, #1126, .F. ) ;
#2853=ORIENTED_EDGE ( 'NONE', *, *, #4636, .T. ) ;
#2855=VERTEX_POINT ( 'NONE', #6958 ) ;
#2856=DIRECTION ( 'NONE',  ( -0.6578909993250587895, -0.7531131608245040798, 0.000000000000000000 ) ) ;
#2861=DIRECTION ( 'NONE',  ( 0.04906492035527378059, -0.9987955914953422498, 0.000000000000000000 ) ) ;
#2865=DIRECTION ( 'NONE',  ( 0.000000000000000000, 0.000000000000000000, -1.000000000000000000 ) ) ;
#2872=ORIENTED_EDGE ( 'NONE', *, *, #3533, .F. ) ;
#2876=ORIENTED_EDGE ( 'NONE', *, *, #469, .T. ) ;
#2878=ORIENTED_EDGE ( 'NONE', *, *, #6250, .F. ) ;
#2884=ADVANCED_FACE ( 'NONE', ( #5769 ), #1878, .T. ) ;
#2885=ADVANCED_FACE ( 'NONE', ( #6422 ), #804, .F. ) ;
#2890=CARTESIAN_POINT ( 'NONE',  ( 1.353740795342265546, 0.002292344206094486941, -0.1250000000000000000 ) ) ;
#2893=DIRECTION ( 'NONE',  ( -0.7540216022612861169, 0.6568496200222109227, 0.000000000000000000 ) ) ;
#2895=VERTEX_POINT ( 'NONE', #1457 ) ;
#2897=DIRECTION ( 'NONE',  ( 0.000000000000000000, -0.000000000000000000, -1.000000000000000000 ) ) ;
#2902=AXIS2_PLACEMENT_3D ( 'NONE', #6020, #6790, #3643 ) ;
#2905=DIRECTION ( 'NONE',  ( -1.000000000000000000, 0.000000000000000000, 0.000000000000000000 ) ) ;
#2908=VECTOR ( 'NONE', #2116, 39.37007874015748143 ) ;
#2915=ORIENTED_EDGE ( 'NONE', *, *, #2287, .F. ) ;
#2917=ORIENTED_EDGE ( 'NONE', *, *, #5191, .F. ) ;
#2918=CARTESIAN_POINT ( 'NONE',  ( 0.1250000000000000000, 1.530808498934191509E-17, 0.1250000000000000000 ) ) ;
#2923=ORIENTED_EDGE ( 'NONE', *, *, #578, .T. ) ;
#2931=DIRECTION ( 'NONE',  ( -1.000000000000000000, 0.000000000000000000, 0.000000000000000000 ) ) ;
#2942=VECTOR ( 'NONE', #5455, 39.37007874015748143 ) ;
#2944=DIRECTION ( 'NONE',  ( -0.000000000000000000, -0.000000000000000000, 1.000000000000000000 ) ) ;
#2945=DIRECTION ( 'NONE',  ( -0.000000000000000000, 0.000000000000000000, 1.000000000000000000 ) ) ;
#2946=VERTEX_POINT ( 'NONE', #3964 ) ;
#2951=CARTESIAN_POINT ( 'NONE',  ( 1.353816004522938599, 0.002313473902802895728, 0.000000000000000000 ) ) ;
#2955=ORIENTED_EDGE ( 'NONE', *, *, #1366, .F. ) ;
#2966=DIRECTION ( 'NONE',  ( 0.6568496200222107007, 0.7540216022612862279, -0.000000000000000000 ) ) ;
#2975=VECTOR ( 'NONE', #1491, 39.37007874015748854 ) ;
#2981=EDGE_LOOP ( 'NONE', ( #2872, #4916, #7117, #3491 ) ) ;
#2984=DIRECTION ( 'NONE',  ( 0.7540216022612862279, -0.6568496200222105896, 0.000000000000000000 ) ) ;
#2988=DIRECTION ( 'NONE',  ( 1.000000000000000000, 0.000000000000000000, 0.000000000000000000 ) ) ;
#2991=EDGE_CURVE ( 'NONE', #2750, #845, #3433, .T. ) ;
#2992=ORIENTED_EDGE ( 'NONE', *, *, #2586, .T. ) ;
#2993=DIRECTION ( 'NONE',  ( -0.000000000000000000, -0.000000000000000000, -1.000000000000000000 ) ) ;
#2997=DIRECTION ( 'NONE',  ( 0.7540216022612864499, -0.6568496200222104786, 0.000000000000000000 ) ) ;
#3001=LINE ( 'NONE', #6162, #3482 ) ;
#3002=ORIENTED_EDGE ( 'NONE', *, *, #4851, .F. ) ;
#3003=DIRECTION ( 'NONE',  ( -0.6568496200222107007, -0.7540216022612862279, 0.000000000000000000 ) ) ;
#3004=ORIENTED_EDGE ( 'NONE', *, *, #4989, .F. ) ;
#3006=CARTESIAN_POINT ( 'NONE',  ( -0.9280291358773672394, 0.8548654847802351631, -0.1250000000000000000 ) ) ;
#3008=ORIENTED_EDGE ( 'NONE', *, *, #6903, .T. ) ;
#3013=CARTESIAN_POINT ( 'NONE',  ( -1.763177565995708296, 1.070083551578370207, -0.08100000000000007194 ) ) ;
#3017=FACE_OUTER_BOUND ( 'NONE', #1888, .T. ) ;
#3021=DIRECTION ( 'NONE',  ( -0.6568496200222107007, -0.7540216022612863389, 0.000000000000000000 ) ) ;
#3024=DIRECTION ( 'NONE',  ( 0.6568496200222107007, 0.7540216022612863389, -0.000000000000000000 ) ) ;
#3029=DIRECTION ( 'NONE',  ( -0.6568496200222107007, -0.7540216022612862279, 0.000000000000000000 ) ) ;
#3036=LINE ( 'NONE', #7984, #8009 ) ;
#3047=ORIENTED_EDGE ( 'NONE', *, *, #8090, .F. ) ;
#3052=VECTOR ( 'NONE', #2993, 39.37007874015748143 ) ;
#3053=DIRECTION ( 'NONE',  ( 0.000000000000000000, 0.000000000000000000, 1.000000000000000000 ) ) ;
#3055=FACE_OUTER_BOUND ( 'NONE', #6272, .T. ) ;
#3057=ORIENTED_EDGE ( 'NONE', *, *, #7397, .F. ) ;
#3061=CARTESIAN_POINT ( 'NONE',  ( 0.000000000000000000, 0.000000000000000000, 0.1250000000000000000 ) ) ;
#3068=ADVANCED_FACE ( 'NONE', ( #3358 ), #2118, .F. ) ;
#3087=DIRECTION ( 'NONE',  ( 0.000000000000000000, 0.000000000000000000, -1.000000000000000000 ) ) ;
#3090=CARTESIAN_POINT ( 'NONE',  ( -1.723766588794375387, 1.115324847714046497, 0.1339999999999995361 ) ) ;
#3099=DIRECTION ( 'NONE',  ( -0.6568496200222107007, -0.7540216022612862279, 0.000000000000000000 ) ) ;
#3101=DIRECTION ( 'NONE',  ( -1.000000000000000000, 0.000000000000000000, 0.000000000000000000 ) ) ;
#3103=FACE_OUTER_BOUND ( 'NONE', #4682, .T. ) ;
#3105=ORIENTED_EDGE ( 'NONE', *, *, #1316, .F. ) ;
#3109=AXIS2_PLACEMENT_3D ( 'NONE', #2557, #5799, #1362 ) ;
#3110=AXIS2_PLACEMENT_3D ( 'NONE', #639, #1088, #545 ) ;
#3114=CARTESIAN_POINT ( 'NONE',  ( -2.022862211726251136, 1.296302217412564017, 0.1339999999999995917 ) ) ;
#3115=ORIENTED_EDGE ( 'NONE', *, *, #1078, .F. ) ;
#3118=CARTESIAN_POINT ( 'NONE',  ( 6.067840808230170246, 0.2405569712445295161, 0.1850000000000003586 ) ) ;
#3121=CARTESIAN_POINT ( 'NONE',  ( 4.013019369095008670, -4.147396371033809537, 0.1250000000000000000 ) ) ;
#3127=ORIENTED_EDGE ( 'NONE', *, *, #1481, .T. ) ;
#3138=EDGE_CURVE ( 'NONE', #789, #6271, #7885, .T. ) ;
#3144=ADVANCED_FACE ( 'NONE', ( #6668 ), #6144, .T. ) ;
#3147=ORIENTED_EDGE ( 'NONE', *, *, #7481, .F. ) ;
#3150=CARTESIAN_POINT ( 'NONE',  ( -1.723766588794375387, 1.115324847714046497, -0.08100000000000007194 ) ) ;
#3151=FACE_OUTER_BOUND ( 'NONE', #2398, .T. ) ;
#3153=ORIENTED_EDGE ( 'NONE', *, *, #598, .F. ) ;
#3154=PLANE ( 'NONE',  #700 ) ;
#3156=CARTESIAN_POINT ( 'NONE',  ( -1.983451234524918450, 1.341543513548241418, 0.1339999999999995917 ) ) ;
#3162=DIRECTION ( 'NONE',  ( 0.7540216022612862279, -0.6568496200222105896, 0.000000000000000000 ) ) ;
#3171=ORIENTED_EDGE ( 'NONE', *, *, #1235, .T. ) ;
#3173=( LENGTH_UNIT ( ) NAMED_UNIT ( * ) SI_UNIT ( $, .METRE. ) );
#3180=EDGE_CURVE ( 'NONE', #4881, #761, #5678, .T. ) ;
#3186=LINE ( 'NONE', #649, #2440 ) ;
#3187=EDGE_CURVE ( 'NONE', #7167, #2507, #5519, .T. ) ;
#3188=EDGE_CURVE ( 'NONE', #5187, #6273, #7409, .T. ) ;
#3190=ORIENTED_EDGE ( 'NONE', *, *, #6642, .T. ) ;
#3191=VECTOR ( 'NONE', #6778, 39.37007874015748854 ) ;
#3192=PLANE ( 'NONE',  #5016 ) ;
#3212=ORIENTED_EDGE ( 'NONE', *, *, #1546, .F. ) ;
#3219=PLANE ( 'NONE',  #3109 ) ;
#3220=CARTESIAN_POINT ( 'NONE',  ( 1.472947776714219836, 0.7825821671288679671, 0.1850000000000003586 ) ) ;
#3224=VERTEX_POINT ( 'NONE', #1650 ) ;
#3226=ORIENTED_EDGE ( 'NONE', *, *, #6942, .T. ) ;
#3230=AXIS2_PLACEMENT_3D ( 'NONE', #3713, #4289, #2349 ) ;
#3233=CARTESIAN_POINT ( 'NONE',  ( 2.387087291339119677, -6.013863021948615106, 0.1250000000000000000 ) ) ;
#3234=AXIS2_PLACEMENT_3D ( 'NONE', #977, #4056, #6556 ) ;
#3236=DIRECTION ( 'NONE',  ( -0.7540216022612862279, 0.6568496200222109227, 0.000000000000000000 ) ) ;
#3246=ADVANCED_FACE ( 'NONE', ( #2754 ), #5387, .T. ) ;
#3250=CARTESIAN_POINT ( 'NONE',  ( -2.114821033088378321, 1.190739337094255168, 0.1339999999999995917 ) ) ;
#3252=EDGE_LOOP ( 'NONE', ( #2386, #1616, #7507, #7068 ) ) ;
#3254=CARTESIAN_POINT ( 'NONE',  ( 0.000000000000000000, 0.000000000000000000, -0.1250000000000000000 ) ) ;
#3259=ORIENTED_EDGE ( 'NONE', *, *, #6005, .F. ) ;
#3260=EDGE_CURVE ( 'NONE', #774, #2343, #7631, .T. ) ;
#3261=ORIENTED_EDGE ( 'NONE', *, *, #4536, .F. ) ;
#3264=PLANE ( 'NONE',  #3723 ) ;
#3265=CARTESIAN_POINT ( 'NONE',  ( 2.056298385200680201, 0.7198786976815831906, -0.09374999999999998612 ) ) ;
#3276=ORIENTED_EDGE ( 'NONE', *, *, #7078, .F. ) ;
#3297=ORIENTED_EDGE ( 'NONE', *, *, #7785, .F. ) ;
#3308=CARTESIAN_POINT ( 'NONE',  ( 3.221700243049673507, 0.8684880333666036289, -0.1849999999999999978 ) ) ;
#3318=CARTESIAN_POINT ( 'NONE',  ( -0.1250000000000000000, 0.000000000000000000, 0.1250000000000000000 ) ) ;
#3319=VERTEX_POINT ( 'NONE', #5357 ) ;
#3324=ORIENTED_EDGE ( 'NONE', *, *, #5442, .T. ) ;
#3344=EDGE_CURVE ( 'NONE', #7381, #4612, #1043, .T. ) ;
#3356=CARTESIAN_POINT ( 'NONE',  ( -1.763177565995707630, 1.070083551578369763, -0.08100000000000007194 ) ) ;
#3358=FACE_OUTER_BOUND ( 'NONE', #6812, .T. ) ;
#3361=AXIS2_PLACEMENT_3D ( 'NONE', #1557, #2865, #7207 ) ;
#3369=ORIENTED_EDGE ( 'NONE', *, *, #4091, .F. ) ;
#3376=CARTESIAN_POINT ( 'NONE',  ( -1.543211452806561690, 0.6927940070358462599, 0.1250000000000000000 ) ) ;
#3385=EDGE_CURVE ( 'NONE', #658, #3319, #7435, .T. ) ;
#3391=ADVANCED_FACE ( 'NONE', ( #8031 ), #3666, .T. ) ;
#3402=DIRECTION ( 'NONE',  ( 0.9987955914953423608, 0.04906492035527378059, 0.000000000000000000 ) ) ;
#3410=EDGE_LOOP ( 'NONE', ( #4869, #5613, #7522, #5572, #1317, #3057 ) ) ;
#3412=CARTESIAN_POINT ( 'NONE',  ( -1.601062921509531556, 0.9288608832735947285, -0.08100000000000007194 ) ) ;
#3415=VERTEX_POINT ( 'NONE', #2918 ) ;
#3419=VERTEX_POINT ( 'NONE', #2306 ) ;
#3430=DIRECTION ( 'NONE',  ( 0.6568496200222108117, 0.7540216022612861169, 0.000000000000000000 ) ) ;
#3431=CYLINDRICAL_SURFACE ( 'NONE', #7485, 0.03124999999999999306 ) ;
#3432=ADVANCED_FACE ( 'NONE', ( #7469 ), #4360, .F. ) ;
#3433=LINE ( 'NONE', #190, #6460 ) ;
#3435=AXIS2_PLACEMENT_3D ( 'NONE', #4577, #2861, #6523 ) ;
#3438=CARTESIAN_POINT ( 'NONE',  ( 1.466665248995881354, 0.6909135088951505743, 0.1250000000000000000 ) ) ;
#3445=CIRCLE ( 'NONE', #7371, 0.3099400561648077423 ) ;
#3447=CYLINDRICAL_SURFACE ( 'NONE', #1666, 8.513908398499120622 ) ;
#3468=CARTESIAN_POINT ( 'NONE',  ( -1.411841654243101596, 0.8435981834898315102, 0.1250000000000000000 ) ) ;
#3472=CARTESIAN_POINT ( 'NONE',  ( 6.190221022838899856, 0.4584861219976859026, 5.393636709996481038 ) ) ;
#3479=DIRECTION ( 'NONE',  ( 1.000000000000000000, 1.092739197465705090E-15, 0.000000000000000000 ) ) ;
#3482=VECTOR ( 'NONE', #4229, 39.37007874015748143 ) ;
#3483=ORIENTED_EDGE ( 'NONE', *, *, #5248, .F. ) ;
#3487=VECTOR ( 'NONE', #5334, 39.37007874015748143 ) ;
#3491=ORIENTED_EDGE ( 'NONE', *, *, #3846, .F. ) ;
#3493=AXIS2_PLACEMENT_3D ( 'NONE', #1092, #8042, #2931 ) ;
#3498=PRODUCT_DEFINITION ( 'UNKNOWN', '', #4611, #7276 ) ;
#3508=ORIENTED_EDGE ( 'NONE', *, *, #6491, .F. ) ;
#3516=DIRECTION ( 'NONE',  ( 0.7540216022612867830, -0.6568496200222101455, -1.912293595564982478E-15 ) ) ;
#3517=ORIENTED_EDGE ( 'NONE', *, *, #7785, .T. ) ;
#3519=DIRECTION ( 'NONE',  ( -0.6568496200222107007, -0.7540216022612862279, 0.000000000000000000 ) ) ;
#3521=DIRECTION ( 'NONE',  ( -0.000000000000000000, -0.000000000000000000, 1.000000000000000000 ) ) ;
#3522=DIRECTION ( 'NONE',  ( -0.000000000000000000, -0.000000000000000000, -1.000000000000000000 ) ) ;
#3527=LINE ( 'NONE', #4185, #7431 ) ;
#3533=EDGE_CURVE ( 'NONE', #3419, #6385, #1720, .T. ) ;
#3535=ORIENTED_EDGE ( 'NONE', *, *, #7397, .T. ) ;
#3555=AXIS2_PLACEMENT_3D ( 'NONE', #5720, #6981, #135 ) ;
#3557=CARTESIAN_POINT ( 'NONE',  ( -1.463573652696772642, 0.6234192589057615530, -0.1918577977169502180 ) ) ;
#3566=ORIENTED_EDGE ( 'NONE', *, *, #6494, .F. ) ;
#3577=ORIENTED_EDGE ( 'NONE', *, *, #2015, .T. ) ;
#3578=CARTESIAN_POINT ( 'NONE',  ( -1.332203854133312548, 0.7742234353597469143, -0.1918577977169502180 ) ) ;
#3581=FACE_OUTER_BOUND ( 'NONE', #3410, .T. ) ;
#3585=ORIENTED_EDGE ( 'NONE', *, *, #6491, .T. ) ;
#3605=LINE ( 'NONE', #5522, #4030 ) ;
#3606=DIRECTION ( 'NONE',  ( -0.6568496200222107007, -0.7540216022612862279, 0.000000000000000000 ) ) ;
#3613=CARTESIAN_POINT ( 'NONE',  ( 6.067840808230170246, 0.2405569712445295161, 5.393636709996481038 ) ) ;
#3622=VERTEX_POINT ( 'NONE', #6323 ) ;
#3633=ORIENTED_EDGE ( 'NONE', *, *, #4788, .F. ) ;
#3635=CARTESIAN_POINT ( 'NONE',  ( 6.067385397437120353, 0.2407432673787524013, -0.1250000000000000000 ) ) ;
#3643=DIRECTION ( 'NONE',  ( 1.000000000000000000, 0.000000000000000000, 0.000000000000000000 ) ) ;
#3649=LINE ( 'NONE', #2445, #5329 ) ;
#3658=VERTEX_POINT ( 'NONE', #7622 ) ;
#3662=DIRECTION ( 'NONE',  ( 1.000000000000000000, 0.000000000000000000, 0.000000000000000000 ) ) ;
#3666=CYLINDRICAL_SURFACE ( 'NONE', #8015, 0.2499999999999998057 ) ;
#3674=CARTESIAN_POINT ( 'NONE',  ( -1.855136387357835481, 0.9645206712600612464, -0.2959999999999997078 ) ) ;
#3677=DIRECTION ( 'NONE',  ( 0.000000000000000000, 0.000000000000000000, 1.000000000000000000 ) ) ;
#3678=DIRECTION ( 'NONE',  ( -0.000000000000000000, -0.000000000000000000, -1.000000000000000000 ) ) ;
#3681=CARTESIAN_POINT ( 'NONE',  ( 1.353740795342265546, 0.002292344206094486941, -6.650588809979335118E-06 ) ) ;
#3693=LINE ( 'NONE', #3121, #1767 ) ;
#3698=LINE ( 'NONE', #6201, #4013 ) ;
#3703=AXIS2_PLACEMENT_3D ( 'NONE', #5978, #4087, #6588 ) ;
#3708=CARTESIAN_POINT ( 'NONE',  ( 3.672767723898985537, -8.314396374632453401, 0.1250000000000000000 ) ) ;
#3713=CARTESIAN_POINT ( 'NONE',  ( 6.067840808230170246, 0.2405569712445295161, 0.1850000000000003586 ) ) ;
#3717=CARTESIAN_POINT ( 'NONE',  ( 6.067840808230170246, 0.2405569712445295161, 5.393636709996481038 ) ) ;
#3720=AXIS2_PLACEMENT_3D ( 'NONE', #3578, #2966, #4818 ) ;
#3721=CARTESIAN_POINT ( 'NONE',  ( -0.02822771919328412663, 0.03615965030273324970, 0.1250000000000000000 ) ) ;
#3723=AXIS2_PLACEMENT_3D ( 'NONE', #7120, #146, #5105 ) ;
#3729=B_SPLINE_CURVE_WITH_KNOTS ( 'NONE', 3,
 ( #4125, #6626, #6017, #2890 ),
 .UNSPECIFIED., .F., .F.,
 ( 4, 4 ),
 ( 0.9793902746300136020, 0.9794065391376511887 ),
 .UNSPECIFIED. ) ;
#3734=VERTEX_POINT ( 'NONE', #2112 ) ;
#3738=CARTESIAN_POINT ( 'NONE',  ( -1.411841654243101596, 0.8435981834898315102, 0.1250000000000000000 ) ) ;
#3741=CIRCLE ( 'NONE', #1508, 9.124497838702110286 ) ;
#3742=DIRECTION ( 'NONE',  ( 0.000000000000000000, -0.000000000000000000, 1.000000000000000000 ) ) ;
#3748=ADVANCED_FACE ( 'NONE', ( #143 ), #2030, .T. ) ;
#3750=AXIS2_PLACEMENT_3D ( 'NONE', #6357, #3858, #6286 ) ;
#3755=AXIS2_PLACEMENT_3D ( 'NONE', #7781, #2128, #7819 ) ;
#3763=CIRCLE ( 'NONE', #6519, 0.2515937209583816725 ) ;
#3773=FACE_OUTER_BOUND ( 'NONE', #4785, .T. ) ;
#3776=PLANE ( 'NONE',  #856 ) ;
#3777=CYLINDRICAL_SURFACE ( 'NONE', #493, 0.2499400561648078278 ) ;
#3789=CARTESIAN_POINT ( 'NONE',  ( 0.1743677072153199392, -0.4209564106690024676, 0.1250000000000000000 ) ) ;
#3795=ORIENTED_EDGE ( 'NONE', *, *, #22, .T. ) ;
#3802=CARTESIAN_POINT ( 'NONE',  ( -1.855136387357835481, 0.9645206712600612464, 0.1339999999999995361 ) ) ;
#3805=ORIENTED_EDGE ( 'NONE', *, *, #2287, .T. ) ;
#3807=DIRECTION ( 'NONE',  ( 0.04906492035527430795, -0.9987955914953422498, 0.000000000000000000 ) ) ;
#3819=LINE ( 'NONE', #5709, #5410 ) ;
#3826=EDGE_LOOP ( 'NONE', ( #2992, #75, #4899, #5743, #5851 ) ) ;
#3834=EDGE_LOOP ( 'NONE', ( #7218, #3633 ) ) ;
#3837=ADVANCED_FACE ( 'NONE', ( #5072 ), #6380, .F. ) ;
#3839=EDGE_LOOP ( 'NONE', ( #4789, #902, #1523, #7038, #1315, #5363, #2596, #7215 ) ) ;
#3845=CARTESIAN_POINT ( 'NONE',  ( -0.9157629057885486867, 0.6051665869063995729, -0.09374999999999998612 ) ) ;
#3846=EDGE_CURVE ( 'NONE', #6385, #297, #7072, .T. ) ;
#3848=DIRECTION ( 'NONE',  ( 1.000000000000000000, 0.000000000000000000, 0.000000000000000000 ) ) ;
#3849=AXIS2_PLACEMENT_3D ( 'NONE', #7475, #6863, #15 ) ;
#3850=VECTOR ( 'NONE', #2856, 39.37007874015748854 ) ;
#3852=DIRECTION ( 'NONE',  ( -1.000000000000000000, 0.000000000000000000, -0.000000000000000000 ) ) ;
#3854=DIRECTION ( 'NONE',  ( -0.7540216022612862279, 0.6568496200222107007, 0.000000000000000000 ) ) ;
#3858=DIRECTION ( 'NONE',  ( 0.000000000000000000, 0.000000000000000000, -1.000000000000000000 ) ) ;
#3859=LINE ( 'NONE', #815, #4755 ) ;
#3870=DIRECTION ( 'NONE',  ( 0.6578909993250586785, 0.7531131608245041908, 0.000000000000000000 ) ) ;
#3875=CIRCLE ( 'NONE', #2696, 0.2499999999999998057 ) ;
#3878=EDGE_LOOP ( 'NONE', ( #1915, #1675, #6928, #2459, #1385, #4336 ) ) ;
#3879=VECTOR ( 'NONE', #6963, 39.37007874015748143 ) ;
#3881=CARTESIAN_POINT ( 'NONE',  ( 4.405984854984288823, -2.483262103238899954, 0.09374999999999998612 ) ) ;
#3883=CARTESIAN_POINT ( 'NONE',  ( -1.983451234524918227, 1.341543513548240529, 0.1339999999999995917 ) ) ;
#3886=FACE_OUTER_BOUND ( 'NONE', #532, .T. ) ;
#3887=EDGE_CURVE ( 'NONE', #1539, #7153, #1656, .T. ) ;
#3891=EDGE_CURVE ( 'NONE', #6385, #5439, #355, .T. ) ;
#3904=DIRECTION ( 'NONE',  ( -0.6578909993250587895, -0.7531131608245040798, 0.000000000000000000 ) ) ;
#3907=CARTESIAN_POINT ( 'NONE',  ( 1.275565605498405253, -0.08258253728086821510, 0.1850000000000003586 ) ) ;
#3918=DIRECTION ( 'NONE',  ( 1.000000000000000000, 0.000000000000000000, 0.000000000000000000 ) ) ;
#3923=DIRECTION ( 'NONE',  ( -1.000000000000000000, 0.000000000000000000, 0.000000000000000000 ) ) ;
#3928=CARTESIAN_POINT ( 'NONE',  ( -1.763177565995707630, 1.070083551578369763, 0.1339999999999995361 ) ) ;
#3940=ORIENTED_EDGE ( 'NONE', *, *, #6397, .F. ) ;
#3947=CIRCLE ( 'NONE', #1594, 9.124497838702110286 ) ;
#3948=DIRECTION ( 'NONE',  ( 0.7540216022612863389, -0.6568496200222107007, 0.000000000000000000 ) ) ;
#3953=VECTOR ( 'NONE', #6467, 39.37007874015748143 ) ;
#3954=ORIENTED_EDGE ( 'NONE', *, *, #1311, .F. ) ;
#3964=CARTESIAN_POINT ( 'NONE',  ( -0.9157629057885486867, 0.6051665869063995729, 0.09374999999999998612 ) ) ;
#3966=CIRCLE ( 'NONE', #6199, 0.1250000000000000000 ) ;
#3973=CARTESIAN_POINT ( 'NONE',  ( 6.190240298342082781, 0.4584752965318059093, 0.1850000000000003586 ) ) ;
#3976=DIRECTION ( 'NONE',  ( -0.000000000000000000, -0.000000000000000000, -1.000000000000000000 ) ) ;
#3977=CIRCLE ( 'NONE', #6857, 0.2149999999999995803 ) ;
#3984=CARTESIAN_POINT ( 'NONE',  ( 1.258616367985684104, -0.02482036785324303815, 0.1849999999999999978 ) ) ;
#3988=DIRECTION ( 'NONE',  ( -0.9595416650617119014, -0.2815666759589949275, 0.000000000000000000 ) ) ;
#3991=EDGE_CURVE ( 'NONE', #774, #3622, #265, .T. ) ;
#3997=ADVANCED_FACE ( 'NONE', ( #934 ), #2814, .T. ) ;
#4000=FACE_OUTER_BOUND ( 'NONE', #2211, .T. ) ;
#4007=VECTOR ( 'NONE', #7196, 39.37007874015748854 ) ;
#4009=ORIENTED_EDGE ( 'NONE', *, *, #5191, .T. ) ;
#4013=VECTOR ( 'NONE', #570, 39.37007874015748143 ) ;
#4015=ORIENTED_EDGE ( 'NONE', *, *, #4194, .F. ) ;
#4019=DIRECTION ( 'NONE',  ( 1.000000000000000000, 0.000000000000000000, 0.000000000000000000 ) ) ;
#4023=AXIS2_PLACEMENT_3D ( 'NONE', #3006, #6208, #7508 ) ;
#4029=LINE ( 'NONE', #323, #213 ) ;
#4030=VECTOR ( 'NONE', #1834, 39.37007874015748143 ) ;
#4031=CARTESIAN_POINT ( 'NONE',  ( -1.052129263295328521, 0.6378420796487936917, 0.1250000000000000000 ) ) ;
#4034=FACE_OUTER_BOUND ( 'NONE', #7227, .T. ) ;
#4036=EDGE_LOOP ( 'NONE', ( #1193, #3127, #4557, #7882 ) ) ;
#4038=CARTESIAN_POINT ( 'NONE',  ( 0.000000000000000000, 0.000000000000000000, -0.1250000000000000000 ) ) ;
#4041=ADVANCED_FACE ( 'NONE', ( #1780 ), #6218, .T. ) ;
#4049=ADVANCED_FACE ( 'NONE', ( #6263 ), #5511, .T. ) ;
#4054=EDGE_CURVE ( 'NONE', #4355, #3734, #5306, .T. ) ;
#4056=DIRECTION ( 'NONE',  ( -0.8680936205257663296, 0.4964005096718442922, 0.000000000000000000 ) ) ;
#4061=CARTESIAN_POINT ( 'NONE',  ( 2.054765106439577771, 0.7510910599158125978, -0.09374999999999998612 ) ) ;
#4068=VERTEX_POINT ( 'NONE', #2433 ) ;
#4071=ORIENTED_EDGE ( 'NONE', *, *, #2330, .F. ) ;
#4073=ORIENTED_EDGE ( 'NONE', *, *, #2422, .T. ) ;
#4082=ORIENTED_EDGE ( 'NONE', *, *, #5583, .F. ) ;
#4086=PLANE ( 'NONE',  #2702 ) ;
#4087=DIRECTION ( 'NONE',  ( 0.000000000000000000, 0.000000000000000000, -1.000000000000000000 ) ) ;
#4091=EDGE_CURVE ( 'NONE', #365, #2424, #1106, .T. ) ;
#4092=EDGE_LOOP ( 'NONE', ( #4378, #3805, #6186, #6237 ) ) ;
#4099=DIRECTION ( 'NONE',  ( 0.04906492035527816598, -0.9987955914953420278, 0.000000000000000000 ) ) ;
#4103=LINE ( 'NONE', #4639, #1932 ) ;
#4109=ORIENTED_EDGE ( 'NONE', *, *, #2135, .T. ) ;
#4115=VECTOR ( 'NONE', #7915, 39.37007874015748143 ) ;
#4121=ORIENTED_EDGE ( 'NONE', *, *, #1311, .T. ) ;
#4125=CARTESIAN_POINT ( 'NONE',  ( 1.353816004522938599, 0.002313473902802895728, -0.1250000000000000278 ) ) ;
#4126=VERTEX_POINT ( 'NONE', #509 ) ;
#4128=CIRCLE ( 'NONE', #7267, 0.1250000000000000000 ) ;
#4133=DIRECTION ( 'NONE',  ( 1.000000000000000000, 7.087526815720798773E-15, 0.000000000000000000 ) ) ;
#4139=ORIENTED_EDGE ( 'NONE', *, *, #634, .T. ) ;
#4144=TOROIDAL_SURFACE ( 'NONE', #471, 0.2812500000000000000, 0.03125000000000000000 ) ;
#4147=DIRECTION ( 'NONE',  ( 0.000000000000000000, 0.000000000000000000, -1.000000000000000000 ) ) ;
#4158=AXIS2_PLACEMENT_3D ( 'NONE', #5556, #2388, #4901 ) ;
#4159=ORIENTED_EDGE ( 'NONE', *, *, #4377, .T. ) ;
#4170=ORIENTED_EDGE ( 'NONE', *, *, #6543, .T. ) ;
#4174=VERTEX_POINT ( 'NONE', #671 ) ;
#4185=CARTESIAN_POINT ( 'NONE',  ( -1.561651944308199313, 0.9741021794092714625, -0.08100000000000007194 ) ) ;
#4189=LINE ( 'NONE', #2583, #1515 ) ;
#4194=EDGE_CURVE ( 'NONE', #2343, #7593, #868, .T. ) ;
#4204=CARTESIAN_POINT ( 'NONE',  ( 6.067840808230170246, 0.2405569712445295161, 5.393636709996481038 ) ) ;
#4205=LINE ( 'NONE', #3674, #1261 ) ;
#4206=DIRECTION ( 'NONE',  ( 1.000000000000000000, 0.000000000000000000, 0.000000000000000000 ) ) ;
#4211=ORIENTED_EDGE ( 'NONE', *, *, #11, .F. ) ;
#4218=CARTESIAN_POINT ( 'NONE',  ( -0.02822771919328412663, 0.03615965030273324970, 0.1250000000000000000 ) ) ;
#4226=VERTEX_POINT ( 'NONE', #1288 ) ;
#4229=DIRECTION ( 'NONE',  ( -0.6568496200222107007, -0.7540216022612862279, 0.000000000000000000 ) ) ;
#4235=ORIENTED_EDGE ( 'NONE', *, *, #7078, .T. ) ;
#4236=EDGE_LOOP ( 'NONE', ( #38, #5733, #7463, #5379 ) ) ;
#4245=AXIS2_PLACEMENT_3D ( 'NONE', #2350, #3053, #3101 ) ;
#4281=AXIS2_PLACEMENT_3D ( 'NONE', #2744, #7132, #7052 ) ;
#4283=CARTESIAN_POINT ( 'NONE',  ( -1.763630694164995738, 1.150051601412734215, -0.3269762307749163877 ) ) ;
#4289=DIRECTION ( 'NONE',  ( -0.000000000000000000, -0.000000000000000000, -1.000000000000000000 ) ) ;
#4290=AXIS2_PLACEMENT_3D ( 'NONE', #4829, #7279, #4292 ) ;
#4292=DIRECTION ( 'NONE',  ( -1.000000000000000000, 0.000000000000000000, 0.000000000000000000 ) ) ;
#4303=VERTEX_POINT ( 'NONE', #3412 ) ;
#4309=VERTEX_POINT ( 'NONE', #7093 ) ;
#4313=DIRECTION ( 'NONE',  ( 0.000000000000000000, 0.000000000000000000, -1.000000000000000000 ) ) ;
#4315=ORIENTED_EDGE ( 'NONE', *, *, #4636, .F. ) ;
#4316=DIRECTION ( 'NONE',  ( 1.000000000000000000, 0.000000000000000000, 0.000000000000000000 ) ) ;
#4319=DIRECTION ( 'NONE',  ( 0.000000000000000000, 0.000000000000000000, -1.000000000000000000 ) ) ;
#4322=ORIENTED_EDGE ( 'NONE', *, *, #7537, .T. ) ;
#4323=DIRECTION ( 'NONE',  ( 1.000000000000000000, 0.000000000000000000, 0.000000000000000000 ) ) ;
#4325=CARTESIAN_POINT ( 'NONE',  ( 6.067840808230170246, 0.2405569712445295161, 0.1250000000000004441 ) ) ;
#4329=DIRECTION ( 'NONE',  ( 0.04906492035527430795, -0.9987955914953422498, 0.000000000000000000 ) ) ;
#4332=DIRECTION ( 'NONE',  ( 0.6568496200222107007, 0.7540216022612863389, -0.000000000000000000 ) ) ;
#4333=CARTESIAN_POINT ( 'NONE',  ( 0.1743677072153199392, -0.4209564106690024676, -0.1250000000000000000 ) ) ;
#4336=ORIENTED_EDGE ( 'NONE', *, *, #4690, .T. ) ;
#4338=ORIENTED_EDGE ( 'NONE', *, *, #2659, .T. ) ;
#4343=FACE_OUTER_BOUND ( 'NONE', #4707, .T. ) ;
#4346=EDGE_CURVE ( 'NONE', #365, #81, #7333, .T. ) ;
#4350=CARTESIAN_POINT ( 'NONE',  ( -0.9142296270274463676, 0.5739542246721701657, -0.1250000000000000000 ) ) ;
#4351=LINE ( 'NONE', #6848, #467 ) ;
#4355=VERTEX_POINT ( 'NONE', #7944 ) ;
#4358=DIRECTION ( 'NONE',  ( -1.000000000000000000, 0.000000000000000000, 0.000000000000000000 ) ) ;
#4360=CYLINDRICAL_SURFACE ( 'NONE', #3720, 0.1249999999999999445 ) ;
#4377=EDGE_CURVE ( 'NONE', #7593, #3622, #456, .T. ) ;
#4378=ORIENTED_EDGE ( 'NONE', *, *, #1537, .F. ) ;
#4381=AXIS2_PLACEMENT_3D ( 'NONE', #763, #2682, #5764 ) ;
#4390=EDGE_CURVE ( 'NONE', #2414, #4493, #1596, .T. ) ;
#4393=CYLINDRICAL_SURFACE ( 'NONE', #5731, 0.03124999999999985428 ) ;
#4412=ORIENTED_EDGE ( 'NONE', *, *, #6033, .F. ) ;
#4419=DIRECTION ( 'NONE',  ( 0.2815666759589948720, -0.9595416650617117904, 0.000000000000000000 ) ) ;
#4437=CARTESIAN_POINT ( 'NONE',  ( 1.258671604940865274, -0.02501003737716508274, 0.1850000000000003586 ) ) ;
#4439=LINE ( 'NONE', #1272, #7877 ) ;
#4441=DIRECTION ( 'NONE',  ( -0.000000000000000000, -0.000000000000000000, -1.000000000000000000 ) ) ;
#4447=ADVANCED_FACE ( 'NONE', ( #76 ), #6961, .F. ) ;
#4451=( NAMED_UNIT ( * ) PLANE_ANGLE_UNIT ( ) SI_UNIT ( $, .RADIAN. ) );
#4454=DIRECTION ( 'NONE',  ( 0.000000000000000000, 0.000000000000000000, 1.000000000000000000 ) ) ;
#4462=ORIENTED_EDGE ( 'NONE', *, *, #373, .F. ) ;
#4465=DIRECTION ( 'NONE',  ( -0.000000000000000000, 0.000000000000000000, 1.000000000000000000 ) ) ;
#4469=CYLINDRICAL_SURFACE ( 'NONE', #6885, 9.004497838701041701 ) ;
#4481=DIRECTION ( 'NONE',  ( 0.000000000000000000, 0.000000000000000000, 1.000000000000000000 ) ) ;
#4486=FACE_OUTER_BOUND ( 'NONE', #6067, .T. ) ;
#4491=ADVANCED_FACE ( 'NONE', ( #4920, #4343 ), #3776, .T. ) ;
#4493=VERTEX_POINT ( 'NONE', #2576 ) ;
#4495=ORIENTED_EDGE ( 'NONE', *, *, #3187, .F. ) ;
#4498=CYLINDRICAL_SURFACE ( 'NONE', #6446, 0.4060000000000000830 ) ;
#4510=ORIENTED_EDGE ( 'NONE', *, *, #3138, .F. ) ;
#4511=DIRECTION ( 'NONE',  ( -0.000000000000000000, 0.000000000000000000, -1.000000000000000000 ) ) ;
#4521=ORIENTED_EDGE ( 'NONE', *, *, #5442, .F. ) ;
#4530=ORIENTED_EDGE ( 'NONE', *, *, #2659, .F. ) ;
#4531=EDGE_LOOP ( 'NONE', ( #3212, #4530, #2802, #5730 ) ) ;
#4535=ORIENTED_EDGE ( 'NONE', *, *, #1978, .F. ) ;
#4536=EDGE_CURVE ( 'NONE', #5921, #4769, #3693, .T. ) ;
#4546=LINE ( 'NONE', #5283, #7362 ) ;
#4552=ORIENTED_EDGE ( 'NONE', *, *, #1586, .F. ) ;
#4553=DIRECTION ( 'NONE',  ( -0.000000000000000000, 0.000000000000000000, 1.000000000000000000 ) ) ;
#4557=ORIENTED_EDGE ( 'NONE', *, *, #469, .F. ) ;
#4558=FACE_OUTER_BOUND ( 'NONE', #7096, .T. ) ;
#4563=DIRECTION ( 'NONE',  ( -0.8680936205257657745, 0.4964005096718455690, -1.084872589120758850E-15 ) ) ;
#4568=DIRECTION ( 'NONE',  ( -0.000000000000000000, 0.000000000000000000, -1.000000000000000000 ) ) ;
#4569=VERTEX_POINT ( 'NONE', #565 ) ;
#4571=ORIENTED_EDGE ( 'NONE', *, *, #7986, .T. ) ;
#4572=VERTEX_POINT ( 'NONE', #614 ) ;
#4577=CARTESIAN_POINT ( 'NONE',  ( 2.054765106439577771, 0.7510910599158125978, 0.1250000000000000000 ) ) ;
#4579=DIRECTION ( 'NONE',  ( -1.000000000000000000, 0.000000000000000000, 0.000000000000000000 ) ) ;
#4586=DIRECTION ( 'NONE',  ( 1.000000000000000000, 0.000000000000000000, 0.000000000000000000 ) ) ;
#4587=DIRECTION ( 'NONE',  ( -0.000000000000000000, -0.000000000000000000, -1.000000000000000000 ) ) ;
#4589=EDGE_CURVE ( 'NONE', #4572, #5716, #6228, .T. ) ;
#4602=CARTESIAN_POINT ( 'NONE',  ( -1.723766588794375387, 1.115324847714046497, -0.08100000000000007194 ) ) ;
#4605=LINE ( 'NONE', #6074, #6905 ) ;
#4610=ORIENTED_EDGE ( 'NONE', *, *, #5602, .T. ) ;
#4611=PRODUCT_DEFINITION_FORMATION_WITH_SPECIFIED_SOURCE ( 'ANY', '', #2761, .NOT_KNOWN. ) ;
#4612=VERTEX_POINT ( 'NONE', #4708 ) ;
#4616=CIRCLE ( 'NONE', #6321, 8.573908398499121120 ) ;
#4617=CARTESIAN_POINT ( 'NONE',  ( -1.615754213267370121, 0.7559880647407505316, 0.1720737575213688586 ) ) ;
#4627=CARTESIAN_POINT ( 'NONE',  ( -1.410683006424825692, 0.8425888524880515984, 0.2499905547878000789 ) ) ;
#4633=DIRECTION ( 'NONE',  ( 0.2791259188691606608, 0.9602545086670756236, 0.000000000000000000 ) ) ;
#4634=AXIS2_PLACEMENT_3D ( 'NONE', #2316, #640, #7445 ) ;
#4636=EDGE_CURVE ( 'NONE', #4309, #2414, #1677, .T. ) ;
#4639=CARTESIAN_POINT ( 'NONE',  ( 6.190219624525621356, 0.4584813330253886265, -0.1849999999999999978 ) ) ;
#4648=CARTESIAN_POINT ( 'NONE',  ( 1.258616368121236118, -0.02482036781376564805, -0.1250000000000000000 ) ) ;
#4655=CARTESIAN_POINT ( 'NONE',  ( -1.543211452806561912, 0.6927940070358482583, -0.1250000000000000000 ) ) ;
#4663=ORIENTED_EDGE ( 'NONE', *, *, #989, .F. ) ;
#4665=CARTESIAN_POINT ( 'NONE',  ( -1.542052804988285786, 0.6917846760340663481, 0.2499905547878000789 ) ) ;
#4668=VECTOR ( 'NONE', #4587, 39.37007874015748143 ) ;
#4675=AXIS2_PLACEMENT_3D ( 'NONE', #4665, #1017, #3516 ) ;
#4679=AXIS2_PLACEMENT_3D ( 'NONE', #4963, #7334, #2997 ) ;
#4682=EDGE_LOOP ( 'NONE', ( #7473, #501, #2192, #6497 ) ) ;
#4689=ORIENTED_EDGE ( 'NONE', *, *, #2321, .T. ) ;
#4690=EDGE_CURVE ( 'NONE', #6271, #6313, #7528, .T. ) ;
#4695=EDGE_CURVE ( 'NONE', #6698, #4355, #6635, .T. ) ;
#4701=CARTESIAN_POINT ( 'NONE',  ( 2.387087291339119677, -6.013863021948615106, 0.1250000000000000000 ) ) ;
#4703=DIRECTION ( 'NONE',  ( 0.000000000000000000, -0.000000000000000000, -1.000000000000000000 ) ) ;
#4707=EDGE_LOOP ( 'NONE', ( #1891, #6741, #1838, #3324, #4170, #2323, #7054, #4159, #4322 ) ) ;
#4708=CARTESIAN_POINT ( 'NONE',  ( 6.190240298342080116, 0.4584752965317958062, 0.1250000000000000278 ) ) ;
#4709=DIRECTION ( 'NONE',  ( -0.000000000000000000, -0.000000000000000000, 1.000000000000000000 ) ) ;
#4710=DIRECTION ( 'NONE',  ( -1.000000000000000000, 0.000000000000000000, 0.000000000000000000 ) ) ;
#4714=DIRECTION ( 'NONE',  ( -0.000000000000000000, -0.000000000000000000, -1.000000000000000000 ) ) ;
#4727=ORIENTED_EDGE ( 'NONE', *, *, #3260, .F. ) ;
#4739=CARTESIAN_POINT ( 'NONE',  ( 3.659299226295303686, -8.245510427152350275, -0.1849999999999999978 ) ) ;
#4747=EDGE_CURVE ( 'NONE', #2895, #5391, #5172, .T. ) ;
#4755=VECTOR ( 'NONE', #2053, 39.37007874015748143 ) ;
#4759=DIRECTION ( 'NONE',  ( 0.000000000000000000, 0.000000000000000000, -1.000000000000000000 ) ) ;
#4767=ORIENTED_EDGE ( 'NONE', *, *, #7481, .T. ) ;
#4769=VERTEX_POINT ( 'NONE', #1297 ) ;
#4772=DIRECTION ( 'NONE',  ( -0.04906492035527816598, 0.9987955914953420278, 0.000000000000000000 ) ) ;
#4782=VERTEX_POINT ( 'NONE', #6758 ) ;
#4785=EDGE_LOOP ( 'NONE', ( #988, #699, #4139 ) ) ;
#4786=EDGE_CURVE ( 'NONE', #2414, #6740, #6230, .T. ) ;
#4788=EDGE_CURVE ( 'NONE', #3415, #2344, #4128, .T. ) ;
#4789=ORIENTED_EDGE ( 'NONE', *, *, #3891, .F. ) ;
#4792=AXIS2_PLACEMENT_3D ( 'NONE', #785, #4563, #1940 ) ;
#4794=ADVANCED_FACE ( 'NONE', ( #4986 ), #5568, .T. ) ;
#4810=VECTOR ( 'NONE', #5856, 39.37007874015748143 ) ;
#4818=DIRECTION ( 'NONE',  ( -0.7540216022612855618, 0.6568496200222115888, 0.000000000000000000 ) ) ;
#4826=CARTESIAN_POINT ( 'NONE',  ( -1.723766588794375387, 1.115324847714046497, -0.2959999999999997078 ) ) ;
#4829=CARTESIAN_POINT ( 'NONE',  ( 0.000000000000000000, 0.000000000000000000, 0.1250000000000000000 ) ) ;
#4830=CARTESIAN_POINT ( 'NONE',  ( 3.690413561029368683, -8.374393170229348371, 0.1849999999999999978 ) ) ;
#4832=DIRECTION ( 'NONE',  ( -0.000000000000000000, -0.000000000000000000, -1.000000000000000000 ) ) ;
#4840=ADVANCED_FACE ( 'NONE', ( #26 ), #648, .T. ) ;
#4851=EDGE_CURVE ( 'NONE', #7230, #2575, #6465, .T. ) ;
#4852=ADVANCED_FACE ( 'NONE', ( #5734 ), #3264, .T. ) ;
#4869=ORIENTED_EDGE ( 'NONE', *, *, #5241, .T. ) ;
#4875=ORIENTED_EDGE ( 'NONE', *, *, #2144, .F. ) ;
#4881=VERTEX_POINT ( 'NONE', #4617 ) ;
#4885=VERTEX_POINT ( 'NONE', #6996 ) ;
#4886=FACE_BOUND ( 'NONE', #85, .T. ) ;
#4890=CARTESIAN_POINT ( 'NONE',  ( 0.1250000000000000000, 1.530808498934191509E-17, 0.1250000000000000000 ) ) ;
#4899=ORIENTED_EDGE ( 'NONE', *, *, #2423, .F. ) ;
#4900=DIRECTION ( 'NONE',  ( -0.000000000000000000, 0.000000000000000000, -1.000000000000000000 ) ) ;
#4901=DIRECTION ( 'NONE',  ( 1.000000000000000000, 0.000000000000000000, 0.000000000000000000 ) ) ;
#4903=CARTESIAN_POINT ( 'NONE',  ( 1.353740795342265546, 0.002292344206094486941, -0.1250000000000000000 ) ) ;
#4907=VERTEX_POINT ( 'NONE', #1372 ) ;
#4909=DIRECTION ( 'NONE',  ( -0.6568496200222107007, -0.7540216022612862279, 0.000000000000000000 ) ) ;
#4916=ORIENTED_EDGE ( 'NONE', *, *, #2422, .F. ) ;
#4919=CIRCLE ( 'NONE', #4792, 0.03124999999999997224 ) ;
#4920=FACE_BOUND ( 'NONE', #8019, .T. ) ;
#4927=EDGE_LOOP ( 'NONE', ( #2515, #1237, #7452 ) ) ;
#4931=AXIS2_PLACEMENT_3D ( 'NONE', #7727, #392, #5366 ) ;
#4940=CIRCLE ( 'NONE', #1654, 0.2149999999999995803 ) ;
#4949=EDGE_CURVE ( 'NONE', #5391, #502, #3977, .T. ) ;
#4955=CARTESIAN_POINT ( 'NONE',  ( -1.855136387357835481, 0.9645206712600612464, -0.08100000000000007194 ) ) ;
#4959=VERTEX_POINT ( 'NONE', #976 ) ;
#4960=DIRECTION ( 'NONE',  ( -1.000000000000000000, -8.814117244050663918E-16, 0.000000000000000000 ) ) ;
#4963=CARTESIAN_POINT ( 'NONE',  ( -1.723766588794375387, 1.115324847714046497, -0.08100000000000007194 ) ) ;
#4973=DIRECTION ( 'NONE',  ( 1.000000000000000000, 0.000000000000000000, 0.000000000000000000 ) ) ;
#4975=ORIENTED_EDGE ( 'NONE', *, *, #5900, .T. ) ;
#4977=FACE_OUTER_BOUND ( 'NONE', #8045, .T. ) ;
#4978=CARTESIAN_POINT ( 'NONE',  ( 1.475891671935536609, 0.7226544316391472211, -0.1849999999999999978 ) ) ;
#4981=VERTEX_POINT ( 'NONE', #5934 ) ;
#4986=FACE_OUTER_BOUND ( 'NONE', #2800, .T. ) ;
#4989=EDGE_CURVE ( 'NONE', #1086, #7112, #1485, .T. ) ;
#4991=ORIENTED_EDGE ( 'NONE', *, *, #6003, .T. ) ;
#4997=FACE_OUTER_BOUND ( 'NONE', #4531, .T. ) ;
#4999=ORIENTED_EDGE ( 'NONE', *, *, #3180, .T. ) ;
#5002=CARTESIAN_POINT ( 'NONE',  ( -0.9280291358773672394, 0.8548654847802351631, 0.1250000000000000000 ) ) ;
#5004=VERTEX_POINT ( 'NONE', #6097 ) ;
#5008=VECTOR ( 'NONE', #4313, 39.37007874015748143 ) ;
#5016=AXIS2_PLACEMENT_3D ( 'NONE', #3233, #2644, #3848 ) ;
#5023=VECTOR ( 'NONE', #4832, 39.37007874015748143 ) ;
#5031=EDGE_CURVE ( 'NONE', #4493, #2946, #1234, .T. ) ;
#5035=DIRECTION ( 'NONE',  ( 1.000000000000000000, 0.000000000000000000, 0.000000000000000000 ) ) ;
#5036=EDGE_LOOP ( 'NONE', ( #5256, #1387, #6895, #1190 ) ) ;
#5039=AXIS2_PLACEMENT_3D ( 'NONE', #401, #7822, #1715 ) ;
#5050=CARTESIAN_POINT ( 'NONE',  ( 3.672798492683009286, -8.252032378159654513, -0.1849999999999999978 ) ) ;
#5052=EDGE_CURVE ( 'NONE', #6392, #1869, #1753, .T. ) ;
#5059=CIRCLE ( 'NONE', #1379, 0.2500000000000000555 ) ;
#5070=AXIS2_PLACEMENT_3D ( 'NONE', #6985, #6332, #675 ) ;
#5071=VECTOR ( 'NONE', #7945, 39.37007874015748143 ) ;
#5072=FACE_OUTER_BOUND ( 'NONE', #4036, .T. ) ;
#5083=DIRECTION ( 'NONE',  ( 0.000000000000000000, 0.000000000000000000, -1.000000000000000000 ) ) ;
#5092=ADVANCED_FACE ( 'NONE', ( #1658 ), #7919, .F. ) ;
#5095=ORIENTED_EDGE ( 'NONE', *, *, #5788, .F. ) ;
#5100=ORIENTED_EDGE ( 'NONE', *, *, #7928, .T. ) ;
#5105=DIRECTION ( 'NONE',  ( -0.9987955914953421388, -0.04906492035527518225, 0.000000000000000000 ) ) ;
#5115=DIRECTION ( 'NONE',  ( 0.2791259188691606608, 0.9602545086670756236, 0.000000000000000000 ) ) ;
#5116=VERTEX_POINT ( 'NONE', #7999 ) ;
#5122=CARTESIAN_POINT ( 'NONE',  ( -0.1250000000000000000, 0.000000000000000000, -0.1250000000000000000 ) ) ;
#5131=EDGE_CURVE ( 'NONE', #6877, #4612, #831, .T. ) ;
#5132=( CONVERSION_BASED_UNIT ( 'INCH', #2554 ) LENGTH_UNIT ( ) NAMED_UNIT ( #2419 ) );
#5135=LINE ( 'NONE', #2512, #7815 ) ;
#5136=CARTESIAN_POINT ( 'NONE',  ( 2.387087291339119677, -6.013863021948615106, -0.1250000000000000000 ) ) ;
#5148=CARTESIAN_POINT ( 'NONE',  ( -1.411633252941551175, 0.8434166392007488300, 0.1120558261758404089 ) ) ;
#5149=ORIENTED_EDGE ( 'NONE', *, *, #5900, .F. ) ;
#5151=DIRECTION ( 'NONE',  ( 0.000000000000000000, 0.000000000000000000, -1.000000000000000000 ) ) ;
#5153=AXIS2_PLACEMENT_3D ( 'NONE', #4602, #6330, #3948 ) ;
#5166=EDGE_LOOP ( 'NONE', ( #2447, #20, #6569, #2727 ) ) ;
#5172=CIRCLE ( 'NONE', #7142, 0.2149999999999995803 ) ;
#5176=AXIS2_PLACEMENT_3D ( 'NONE', #3708, #1162, #465 ) ;
#5187=VERTEX_POINT ( 'NONE', #4903 ) ;
#5188=TOROIDAL_SURFACE ( 'NONE', #744, 0.2812500000000000000, 0.03125000000000000000 ) ;
#5190=ORIENTED_EDGE ( 'NONE', *, *, #5839, .T. ) ;
#5191=EDGE_CURVE ( 'NONE', #158, #4569, #7772, .T. ) ;
#5201=CYLINDRICAL_SURFACE ( 'NONE', #1072, 0.2499962251234248700 ) ;
#5216=DIRECTION ( 'NONE',  ( 0.7540216022612861169, -0.6568496200222107007, 0.000000000000000000 ) ) ;
#5230=DIRECTION ( 'NONE',  ( 1.000000000000000000, 0.000000000000000000, 0.000000000000000000 ) ) ;
#5231=DIRECTION ( 'NONE',  ( -0.000000000000000000, -0.000000000000000000, -1.000000000000000000 ) ) ;
#5238=VERTEX_POINT ( 'NONE', #4978 ) ;
#5241=EDGE_CURVE ( 'NONE', #4782, #4572, #5296, .T. ) ;
#5242=LINE ( 'NONE', #6557, #2908 ) ;
#5246=ADVANCED_FACE ( 'NONE', ( #4000 ), #1321, .F. ) ;
#5248=EDGE_CURVE ( 'NONE', #2855, #5686, #574, .T. ) ;
#5251=CARTESIAN_POINT ( 'NONE',  ( 3.690413561029368683, -8.374393170229348371, 0.1250000000000000000 ) ) ;
#5253=DIRECTION ( 'NONE',  ( -0.6568496200222107007, -0.7540216022612863389, 0.000000000000000000 ) ) ;
#5256=ORIENTED_EDGE ( 'NONE', *, *, #5241, .F. ) ;
#5257=DIRECTION ( 'NONE',  ( -1.000000000000000000, 0.000000000000000000, 0.000000000000000000 ) ) ;
#5259=LINE ( 'NONE', #205, #7549 ) ;
#5261=ORIENTED_EDGE ( 'NONE', *, *, #4949, .F. ) ;
#5267=DIRECTION ( 'NONE',  ( -1.000000000000000000, 0.000000000000000000, 0.000000000000000000 ) ) ;
#5274=AXIS2_PLACEMENT_3D ( 'NONE', #7848, #6057, #2893 ) ;
#5276=B_SPLINE_CURVE_WITH_KNOTS ( 'NONE', 3,
 ( #2840, #7753, #2142, #4648 ),
 .UNSPECIFIED., .F., .F.,
 ( 4, 4 ),
 ( 0.9794065391376511887, 1.000000000000000000 ),
 .UNSPECIFIED. ) ;
#5279=DIRECTION ( 'NONE',  ( 0.000000000000000000, 0.000000000000000000, -1.000000000000000000 ) ) ;
#5280=EDGE_LOOP ( 'NONE', ( #4315, #5886, #1012, #6622 ) ) ;
#5282=FACE_OUTER_BOUND ( 'NONE', #2981, .T. ) ;
#5283=CARTESIAN_POINT ( 'NONE',  ( 1.258616367985684104, -0.02482036785324303815, 0.1849999999999999978 ) ) ;
#5296=CIRCLE ( 'NONE', #3849, 9.064497838702109789 ) ;
#5303=EDGE_LOOP ( 'NONE', ( #3190, #1146, #3261, #1693 ) ) ;
#5306=CIRCLE ( 'NONE', #61, 0.2499962251234248700 ) ;
#5325=DIRECTION ( 'NONE',  ( 1.000000000000000000, 0.000000000000000000, 0.000000000000000000 ) ) ;
#5329=VECTOR ( 'NONE', #2944, 39.37007874015748143 ) ;
#5333=DIRECTION ( 'NONE',  ( 0.7540216022612865610, -0.6568496200222104786, 0.000000000000000000 ) ) ;
#5334=DIRECTION ( 'NONE',  ( -0.000000000000000000, -0.000000000000000000, -1.000000000000000000 ) ) ;
#5335=ORIENTED_EDGE ( 'NONE', *, *, #6506, .T. ) ;
#5337=AXIS2_PLACEMENT_3D ( 'NONE', #3717, #8001, #7447 ) ;
#5342=CIRCLE ( 'NONE', #6645, 9.064497838702109789 ) ;
#5343=CARTESIAN_POINT ( 'NONE',  ( 3.659299226295303686, -8.245510427152350275, 0.1850000000000003586 ) ) ;
#5352=ORIENTED_EDGE ( 'NONE', *, *, #7938, .T. ) ;
#5357=CARTESIAN_POINT ( 'NONE',  ( -1.983451234524918450, 1.341543513548241418, -0.2959999999999997078 ) ) ;
#5363=ORIENTED_EDGE ( 'NONE', *, *, #4690, .F. ) ;
#5365=CARTESIAN_POINT ( 'NONE',  ( 3.672798492683009286, -8.252032378159654513, 0.1850000000000003586 ) ) ;
#5366=DIRECTION ( 'NONE',  ( 0.2791259188691606608, 0.9602545086670756236, 0.000000000000000000 ) ) ;
#5367=EDGE_LOOP ( 'NONE', ( #4991, #895, #1302, #6550 ) ) ;
#5369=CARTESIAN_POINT ( 'NONE',  ( 0.000000000000000000, 0.000000000000000000, 0.1250000000000000000 ) ) ;
#5374=VERTEX_POINT ( 'NONE', #5796 ) ;
#5375=DIRECTION ( 'NONE',  ( 0.000000000000000000, 0.000000000000000000, -1.000000000000000000 ) ) ;
#5377=LINE ( 'NONE', #2795, #5071 ) ;
#5379=ORIENTED_EDGE ( 'NONE', *, *, #215, .F. ) ;
#5382=VERTEX_POINT ( 'NONE', #2672 ) ;
#5387=PLANE ( 'NONE',  #7250 ) ;
#5391=VERTEX_POINT ( 'NONE', #258 ) ;
#5410=VECTOR ( 'NONE', #5216, 39.37007874015748854 ) ;
#5411=CYLINDRICAL_SURFACE ( 'NONE', #1742, 8.696493751522730520 ) ;
#5417=LINE ( 'NONE', #7308, #600 ) ;
#5423=ORIENTED_EDGE ( 'NONE', *, *, #3344, .T. ) ;
#5428=DIRECTION ( 'NONE',  ( -1.000000000000000000, 0.000000000000000000, 0.000000000000000000 ) ) ;
#5439=VERTEX_POINT ( 'NONE', #4655 ) ;
#5442=EDGE_CURVE ( 'NONE', #5238, #4885, #1572, .T. ) ;
#5443=AXIS2_PLACEMENT_3D ( 'NONE', #6087, #5508, #4973 ) ;
#5445=CARTESIAN_POINT ( 'NONE',  ( 6.317381622560545473, 0.2407432673787524013, -0.1849999999999999978 ) ) ;
#5450=AXIS2_PLACEMENT_3D ( 'NONE', #5002, #5083, #6930 ) ;
#5455=DIRECTION ( 'NONE',  ( -0.000000000000000000, -0.000000000000000000, 1.000000000000000000 ) ) ;
#5456=DIRECTION ( 'NONE',  ( 0.9987955914953421388, 0.04906492035527377366, -0.000000000000000000 ) ) ;
#5463=FACE_OUTER_BOUND ( 'NONE', #2208, .T. ) ;
#5464=CIRCLE ( 'NONE', #1268, 9.004497838701041701 ) ;
#5465=ORIENTED_EDGE ( 'NONE', *, *, #7439, .F. ) ;
#5467=ORIENTED_EDGE ( 'NONE', *, *, #1479, .T. ) ;
#5474=DIRECTION ( 'NONE',  ( -1.000000000000000000, 0.000000000000000000, 0.000000000000000000 ) ) ;
#5477=CYLINDRICAL_SURFACE ( 'NONE', #3493, 9.064497838702109789 ) ;
#5478=DIRECTION ( 'NONE',  ( -0.6568496200222107007, -0.7540216022612862279, 0.000000000000000000 ) ) ;
#5489=CARTESIAN_POINT ( 'NONE',  ( -0.9280291358773672394, 0.8548654847802351631, -0.09374999999999998612 ) ) ;
#5490=ORIENTED_EDGE ( 'NONE', *, *, #1080, .F. ) ;
#5496=DIRECTION ( 'NONE',  ( 0.2791259188691606608, 0.9602545086670756236, 0.000000000000000000 ) ) ;
#5500=CARTESIAN_POINT ( 'NONE',  ( 1.472069962421741263, 0.7095069109563477694, -0.1249999999999999306 ) ) ;
#5508=DIRECTION ( 'NONE',  ( -0.000000000000000000, 0.000000000000000000, 1.000000000000000000 ) ) ;
#5509=ORIENTED_EDGE ( 'NONE', *, *, #6840, .T. ) ;
#5511=CYLINDRICAL_SURFACE ( 'NONE', #2157, 0.2499962251234248700 ) ;
#5512=DIRECTION ( 'NONE',  ( -0.7540216022612862279, 0.6568496200222109227, 0.000000000000000000 ) ) ;
#5519=LINE ( 'NONE', #8007, #6069 ) ;
#5522=CARTESIAN_POINT ( 'NONE',  ( 6.000000000000001776, 0.000000000000000000, 5.393636709996481038 ) ) ;
#5524=DIRECTION ( 'NONE',  ( 1.000000000000000000, 0.000000000000000000, 0.000000000000000000 ) ) ;
#5532=DIRECTION ( 'NONE',  ( -0.000000000000000000, -0.000000000000000000, -1.000000000000000000 ) ) ;
#5536=CARTESIAN_POINT ( 'NONE',  ( 1.475891671935536609, 0.7226544316391472211, -0.09375000000000005551 ) ) ;
#5543=EDGE_CURVE ( 'NONE', #4068, #91, #5342, .T. ) ;
#5544=DIRECTION ( 'NONE',  ( -0.000000000000000000, 0.000000000000000000, 1.000000000000000000 ) ) ;
#5550=EDGE_CURVE ( 'NONE', #2946, #4309, #5915, .T. ) ;
#5556=CARTESIAN_POINT ( 'NONE',  ( 3.666415866878782737, -8.185094079965432812, 0.1250000000000000000 ) ) ;
#5566=VECTOR ( 'NONE', #3678, 39.37007874015748143 ) ;
#5568=CYLINDRICAL_SURFACE ( 'NONE', #6336, 0.4999999999999997224 ) ;
#5572=ORIENTED_EDGE ( 'NONE', *, *, #4054, .F. ) ;
#5577=DIRECTION ( 'NONE',  ( 0.000000000000000000, 0.000000000000000000, -1.000000000000000000 ) ) ;
#5583=EDGE_CURVE ( 'NONE', #4303, #5391, #3527, .T. ) ;
#5586=CIRCLE ( 'NONE', #3755, 0.2499962251234248700 ) ;
#5594=PLANE ( 'NONE',  #5443 ) ;
#5595=EDGE_CURVE ( 'NONE', #7842, #3419, #5377, .T. ) ;
#5602=EDGE_CURVE ( 'NONE', #796, #4126, #4103, .T. ) ;
#5608=DIRECTION ( 'NONE',  ( -1.000000000000000000, -7.137164547826461966E-15, 0.000000000000000000 ) ) ;
#5609=CIRCLE ( 'NONE', #2706, 8.696493751522730520 ) ;
#5613=ORIENTED_EDGE ( 'NONE', *, *, #4589, .T. ) ;
#5620=DIRECTION ( 'NONE',  ( 0.7540216022612862279, -0.6568496200222107007, 0.000000000000000000 ) ) ;
#5623=ORIENTED_EDGE ( 'NONE', *, *, #5543, .F. ) ;
#5627=CARTESIAN_POINT ( 'NONE',  ( 3.672798492683009286, -8.252032378159654513, 0.1250000000000004441 ) ) ;
#5636=ADVANCED_FACE ( 'NONE', ( #4034 ), #3447, .F. ) ;
#5646=EDGE_CURVE ( 'NONE', #963, #8047, #6535, .T. ) ;
#5647=ADVANCED_FACE ( 'NONE', ( #1188 ), #6884, .F. ) ;
#5649=DIRECTION ( 'NONE',  ( -0.6568496200222107007, -0.7540216022612862279, 0.000000000000000000 ) ) ;
#5665=CARTESIAN_POINT ( 'NONE',  ( -1.411633252941551397, 0.8434166392007489410, -0.09374999999999998612 ) ) ;
#5667=AXIS2_PLACEMENT_3D ( 'NONE', #1389, #6288, #5747 ) ;
#5673=CARTESIAN_POINT ( 'NONE',  ( -1.411841654243101596, 0.8435981834898315102, -0.1250000000000000000 ) ) ;
#5675=ORIENTED_EDGE ( 'NONE', *, *, #1546, .T. ) ;
#5678=CIRCLE ( 'NONE', #2526, 0.4060000000000001386 ) ;
#5683=AXIS2_PLACEMENT_3D ( 'NONE', #4325, #6137, #1131 ) ;
#5686=VERTEX_POINT ( 'NONE', #3156 ) ;
#5694=EDGE_CURVE ( 'NONE', #3319, #3658, #8070, .T. ) ;
#5697=AXIS2_PLACEMENT_3D ( 'NONE', #5136, #139, #2595 ) ;
#5700=ADVANCED_FACE ( 'NONE', ( #6842 ), #3777, .F. ) ;
#5703=FACE_OUTER_BOUND ( 'NONE', #5303, .T. ) ;
#5705=ORIENTED_EDGE ( 'NONE', *, *, #4695, .T. ) ;
#5709=CARTESIAN_POINT ( 'NONE',  ( -1.763177565995707630, 1.070083551578369763, 0.1339999999999995361 ) ) ;
#5715=VECTOR ( 'NONE', #3606, 39.37007874015748143 ) ;
#5716=VERTEX_POINT ( 'NONE', #2365 ) ;
#5719=ORIENTED_EDGE ( 'NONE', *, *, #11, .T. ) ;
#5720=CARTESIAN_POINT ( 'NONE',  ( 0.000000000000000000, 0.000000000000000000, 0.000000000000000000 ) ) ;
#5721=ORIENTED_EDGE ( 'NONE', *, *, #6181, .F. ) ;
#5725=DIRECTION ( 'NONE',  ( 1.000000000000000000, 0.000000000000000000, 0.000000000000000000 ) ) ;
#5728=CIRCLE ( 'NONE', #4158, 9.004497838701041701 ) ;
#5730=ORIENTED_EDGE ( 'NONE', *, *, #6393, .F. ) ;
#5731=AXIS2_PLACEMENT_3D ( 'NONE', #6281, #656, #6158 ) ;
#5733=ORIENTED_EDGE ( 'NONE', *, *, #5583, .T. ) ;
#5734=FACE_OUTER_BOUND ( 'NONE', #2633, .T. ) ;
#5736=CARTESIAN_POINT ( 'NONE',  ( -1.411633252941551619, 0.8434166392007494961, 0.09374999999999998612 ) ) ;
#5741=CARTESIAN_POINT ( 'NONE',  ( -1.543211452806561912, 0.6927940070358482583, 0.1250000000000000000 ) ) ;
#5743=ORIENTED_EDGE ( 'NONE', *, *, #1085, .F. ) ;
#5745=CARTESIAN_POINT ( 'NONE',  ( 3.666415866878782737, -8.185094079965432812, 0.1849999999999999978 ) ) ;
#5747=DIRECTION ( 'NONE',  ( 1.000000000000000000, 1.417505363144159755E-14, 0.000000000000000000 ) ) ;
#5754=ORIENTED_EDGE ( 'NONE', *, *, #5543, .T. ) ;
#5756=EDGE_LOOP ( 'NONE', ( #6387, #7616, #7859, #1712 ) ) ;
#5762=ORIENTED_EDGE ( 'NONE', *, *, #7827, .F. ) ;
#5764=DIRECTION ( 'NONE',  ( -0.9968059542140785823, 0.000000000000000000, 0.07986169071188248259 ) ) ;
#5765=ORIENTED_EDGE ( 'NONE', *, *, #3887, .T. ) ;
#5768=LINE ( 'NONE', #7488, #6968 ) ;
#5769=FACE_OUTER_BOUND ( 'NONE', #7416, .T. ) ;
#5776=CYLINDRICAL_SURFACE ( 'NONE', #5450, 0.2500000000000000555 ) ;
#5781=CARTESIAN_POINT ( 'NONE',  ( -1.420319797626316438, 0.8334728170008731674, -0.1249999999999997641 ) ) ;
#5783=( GEOMETRIC_REPRESENTATION_CONTEXT ( 3 ) GLOBAL_UNCERTAINTY_ASSIGNED_CONTEXT ( ( #390 ) ) GLOBAL_UNIT_ASSIGNED_CONTEXT ( ( #5132, #4451, #6946 ) ) REPRESENTATION_CONTEXT ( 'NONE', 'WORKASPACE' ) );
#5788=EDGE_CURVE ( 'NONE', #8047, #1448, #5609, .T. ) ;
#5795=DIRECTION ( 'NONE',  ( -0.000000000000000000, 0.000000000000000000, 1.000000000000000000 ) ) ;
#5796=CARTESIAN_POINT ( 'NONE',  ( 0.1250000000000000000, 1.530808498934191509E-17, -0.1250000000000000000 ) ) ;
#5799=DIRECTION ( 'NONE',  ( 0.000000000000000000, 0.000000000000000000, 1.000000000000000000 ) ) ;
#5802=AXIS2_PLACEMENT_3D ( 'NONE', #6433, #87, #122 ) ;
#5804=CIRCLE ( 'NONE', #7110, 0.2499400561648078278 ) ;
#5808=CARTESIAN_POINT ( 'NONE',  ( -1.763177565995707630, 1.070083551578369763, -0.2959999999999997078 ) ) ;
#5811=AXIS2_PLACEMENT_3D ( 'NONE', #7126, #1507, #4019 ) ;
#5815=LINE ( 'NONE', #7655, #3879 ) ;
#5820=ORIENTED_EDGE ( 'NONE', *, *, #6807, .T. ) ;
#5827=ADVANCED_FACE ( 'NONE', ( #4997 ), #4393, .T. ) ;
#5828=ORIENTED_EDGE ( 'NONE', *, *, #5602, .F. ) ;
#5833=ORIENTED_EDGE ( 'NONE', *, *, #7459, .T. ) ;
#5839=EDGE_CURVE ( 'NONE', #2344, #3415, #602, .T. ) ;
#5844=EDGE_CURVE ( 'NONE', #4881, #2855, #5815, .T. ) ;
#5845=VERTEX_POINT ( 'NONE', #3928 ) ;
#5848=AXIS2_PLACEMENT_3D ( 'NONE', #6478, #811, #2000 ) ;
#5851=ORIENTED_EDGE ( 'NONE', *, *, #6204, .T. ) ;
#5856=DIRECTION ( 'NONE',  ( 0.9987955914953421388, 0.04906492035527518225, -0.000000000000000000 ) ) ;
#5861=VECTOR ( 'NONE', #758, 39.37007874015748143 ) ;
#5867=PLANE ( 'NONE',  #7301 ) ;
#5877=ORIENTED_EDGE ( 'NONE', *, *, #6589, .T. ) ;
#5881=CARTESIAN_POINT ( 'NONE',  ( 1.475891671935536609, 0.7226544316391472211, -0.1849999999999999978 ) ) ;
#5886=ORIENTED_EDGE ( 'NONE', *, *, #5550, .F. ) ;
#5887=ADVANCED_FACE ( 'NONE', ( #5703 ), #7006, .F. ) ;
#5897=DIRECTION ( 'NONE',  ( -0.6568496200222107007, -0.7540216022612862279, 0.000000000000000000 ) ) ;
#5900=EDGE_CURVE ( 'NONE', #7153, #1621, #208, .T. ) ;
#5915=LINE ( 'NONE', #289, #2450 ) ;
#5920=DIRECTION ( 'NONE',  ( 0.000000000000000000, 0.000000000000000000, -1.000000000000000000 ) ) ;
#5921=VERTEX_POINT ( 'NONE', #5741 ) ;
#5934=CARTESIAN_POINT ( 'NONE',  ( 3.221700243049673507, 0.8684880333666047392, 0.1850000000000003586 ) ) ;
#5937=DIRECTION ( 'NONE',  ( -0.2791259188691606608, -0.9602545086670756236, -0.000000000000000000 ) ) ;
#5943=LINE ( 'NONE', #5987, #1781 ) ;
#5955=DIRECTION ( 'NONE',  ( 0.7540216022612858948, -0.6568496200222110337, 0.000000000000000000 ) ) ;
#5959=EDGE_LOOP ( 'NONE', ( #4211, #6056, #3566, #4663 ) ) ;
#5961=ORIENTED_EDGE ( 'NONE', *, *, #1284, .T. ) ;
#5970=ORIENTED_EDGE ( 'NONE', *, *, #6257, .T. ) ;
#5977=CIRCLE ( 'NONE', #86, 0.1250000000000001388 ) ;
#5978=CARTESIAN_POINT ( 'NONE',  ( 3.672798492683009286, -8.252032378159654513, 5.393636709996481038 ) ) ;
#5980=CIRCLE ( 'NONE', #736, 0.1249999999999999029 ) ;
#5981=ORIENTED_EDGE ( 'NONE', *, *, #3991, .T. ) ;
#5984=PRODUCT_DEFINITION_SHAPE ( 'NONE', 'NONE',  #3498 ) ;
#5987=CARTESIAN_POINT ( 'NONE',  ( -1.763630694164994850, 1.150051601412733771, 0.1649762307749162715 ) ) ;
#5988=ORIENTED_EDGE ( 'NONE', *, *, #6298, .F. ) ;
#5996=VECTOR ( 'NONE', #4147, 39.37007874015748143 ) ;
#6003=EDGE_CURVE ( 'NONE', #6740, #1607, #6246, .T. ) ;
#6005=EDGE_CURVE ( 'NONE', #1614, #4959, #5059, .T. ) ;
#6012=CARTESIAN_POINT ( 'NONE',  ( -1.803041671366328202, 1.104810305277057259, -0.3269762307749163877 ) ) ;
#6017=CARTESIAN_POINT ( 'NONE',  ( 1.353765837681602191, 0.002299485657152759710, -0.1250000000000000278 ) ) ;
#6020=CARTESIAN_POINT ( 'NONE',  ( 6.067386035484801710, 0.2407470087491039856, 0.1250000000000000000 ) ) ;
#6021=DIRECTION ( 'NONE',  ( -0.000000000000000000, -0.000000000000000000, 1.000000000000000000 ) ) ;
#6023=CARTESIAN_POINT ( 'NONE',  ( 6.067385397437120353, 0.2407432673787524013, -0.1849999999999999978 ) ) ;
#6024=FACE_OUTER_BOUND ( 'NONE', #1173, .T. ) ;
#6030=ORIENTED_EDGE ( 'NONE', *, *, #4589, .F. ) ;
#6033=EDGE_CURVE ( 'NONE', #5382, #1614, #7733, .T. ) ;
#6056=ORIENTED_EDGE ( 'NONE', *, *, #5844, .F. ) ;
#6057=DIRECTION ( 'NONE',  ( 0.6568496200222107007, 0.7540216022612863389, 0.000000000000000000 ) ) ;
#6067=EDGE_LOOP ( 'NONE', ( #613, #2602, #4109, #346 ) ) ;
#6069=VECTOR ( 'NONE', #2396, 39.37007874015748854 ) ;
#6071=DIRECTION ( 'NONE',  ( -0.6568496200222107007, -0.7540216022612862279, 0.000000000000000000 ) ) ;
#6074=CARTESIAN_POINT ( 'NONE',  ( -1.411841654243101596, 0.8435981834898315102, -0.1250000000000000000 ) ) ;
#6083=CARTESIAN_POINT ( 'NONE',  ( 6.190240298342082781, 0.4584752965318060758, 0.000000000000000000 ) ) ;
#6087=CARTESIAN_POINT ( 'NONE',  ( 2.387087291339119677, -6.013863021948615106, -0.1250000000000000000 ) ) ;
#6089=CLOSED_SHELL ( 'NONE', ( #4447, #6828, #816, #586, #6587, #1629, #4840, #2426, #3144, #1819, #3432, #7943, #7392, #3837, #7101 ) ) ;
#6090=VECTOR ( 'NONE', #2747, 39.37007874015748143 ) ;
#6094=EDGE_CURVE ( 'NONE', #6811, #7764, #2213, .T. ) ;
#6097=CARTESIAN_POINT ( 'NONE',  ( -0.3566525292043903339, -0.3408511508279103985, -0.1250000000000000000 ) ) ;
#6100=DIRECTION ( 'NONE',  ( -1.000000000000000000, 0.000000000000000000, 0.000000000000000000 ) ) ;
#6101=VECTOR ( 'NONE', #2231, 39.37007874015748143 ) ;
#6106=ADVANCED_FACE ( 'NONE', ( #7176 ), #7779, .T. ) ;
#6110=CARTESIAN_POINT ( 'NONE',  ( 1.353740795342264880, 0.002292344206096672693, 0.1250000000000592026 ) ) ;
#6113=ORIENTED_EDGE ( 'NONE', *, *, #4377, .F. ) ;
#6118=CARTESIAN_POINT ( 'NONE',  ( -0.9142296270274480330, 0.5739542246721696106, 0.1250000000000000000 ) ) ;
#6125=DIRECTION ( 'NONE',  ( -0.000000000000000000, 0.000000000000000000, -1.000000000000000000 ) ) ;
#6134=ORIENTED_EDGE ( 'NONE', *, *, #7085, .F. ) ;
#6137=DIRECTION ( 'NONE',  ( 0.000000000000000000, -0.000000000000000000, -1.000000000000000000 ) ) ;
#6144=PLANE ( 'NONE',  #443 ) ;
#6151=ORIENTED_EDGE ( 'NONE', *, *, #1235, .F. ) ;
#6156=EDGE_CURVE ( 'NONE', #713, #3658, #5977, .T. ) ;
#6158=DIRECTION ( 'NONE',  ( 0.4964005096718474008, 0.8680936205257645533, 0.000000000000000000 ) ) ;
#6162=CARTESIAN_POINT ( 'NONE',  ( -1.411841654243101596, 0.8435981834898315102, 0.1250000000000000000 ) ) ;
#6167=DIRECTION ( 'NONE',  ( -0.000000000000000000, -0.000000000000000000, -1.000000000000000000 ) ) ;
#6171=ORIENTED_EDGE ( 'NONE', *, *, #4695, .F. ) ;
#6172=ORIENTED_EDGE ( 'NONE', *, *, #3188, .F. ) ;
#6181=EDGE_CURVE ( 'NONE', #6698, #898, #1136, .T. ) ;
#6186=ORIENTED_EDGE ( 'NONE', *, *, #215, .T. ) ;
#6188=LINE ( 'NONE', #1220, #3052 ) ;
#6189=CIRCLE ( 'NONE', #7229, 0.03124999999999999306 ) ;
#6199=AXIS2_PLACEMENT_3D ( 'NONE', #4038, #7186, #2300 ) ;
#6200=FACE_OUTER_BOUND ( 'NONE', #677, .T. ) ;
#6201=CARTESIAN_POINT ( 'NONE',  ( 6.185915932928153005, 0.4597367884986204856, 0.000000000000000000 ) ) ;
#6204=EDGE_CURVE ( 'NONE', #2424, #6313, #3649, .T. ) ;
#6206=AXIS2_PLACEMENT_3D ( 'NONE', #5369, #6524, #4579 ) ;
#6208=DIRECTION ( 'NONE',  ( -0.000000000000000000, 0.000000000000000000, 1.000000000000000000 ) ) ;
#6213=VECTOR ( 'NONE', #3087, 39.37007874015748143 ) ;
#6215=AXIS2_PLACEMENT_3D ( 'NONE', #5365, #1090, #310 ) ;
#6218=CYLINDRICAL_SURFACE ( 'NONE', #7777, 0.3099400561648077423 ) ;
#6223=CARTESIAN_POINT ( 'NONE',  ( 1.258616367985684104, -0.02482036785324303815, 0.1250000000000000000 ) ) ;
#6228=CIRCLE ( 'NONE', #7396, 0.2499400561648078278 ) ;
#6229=ORIENTED_EDGE ( 'NONE', *, *, #3891, .T. ) ;
#6230=LINE ( 'NONE', #519, #7653 ) ;
#6233=ORIENTED_EDGE ( 'NONE', *, *, #2991, .T. ) ;
#6234=ORIENTED_EDGE ( 'NONE', *, *, #6494, .T. ) ;
#6237=ORIENTED_EDGE ( 'NONE', *, *, #6840, .F. ) ;
#6245=ORIENTED_EDGE ( 'NONE', *, *, #2374, .F. ) ;
#6246=CIRCLE ( 'NONE', #7546, 8.696493751522730520 ) ;
#6250=EDGE_CURVE ( 'NONE', #375, #658, #3763, .T. ) ;
#6253=CIRCLE ( 'NONE', #8055, 0.3099400561648077423 ) ;
#6257=EDGE_CURVE ( 'NONE', #5116, #340, #3605, .T. ) ;
#6263=FACE_OUTER_BOUND ( 'NONE', #7714, .T. ) ;
#6269=AXIS2_PLACEMENT_3D ( 'NONE', #7498, #530, #5496 ) ;
#6270=CARTESIAN_POINT ( 'NONE',  ( 6.068104892000602213, -0.009251957739379222667, 0.1849999999999999978 ) ) ;
#6271=VERTEX_POINT ( 'NONE', #4333 ) ;
#6272=EDGE_LOOP ( 'NONE', ( #3954, #5335, #3115, #5623 ) ) ;
#6273=VERTEX_POINT ( 'NONE', #6110 ) ;
#6275=LINE ( 'NONE', #3881, #6633 ) ;
#6279=ORIENTED_EDGE ( 'NONE', *, *, #6807, .F. ) ;
#6281=CARTESIAN_POINT ( 'NONE',  ( 4.390472339057043705, -2.510390028880329805, 0.09374999999999998612 ) ) ;
#6283=ORIENTED_EDGE ( 'NONE', *, *, #1577, .T. ) ;
#6285=MANIFOLD_SOLID_BREP ( 'Cut-Extrude1', #6089 ) ;
#6286=DIRECTION ( 'NONE',  ( -1.000000000000000000, 0.000000000000000000, 0.000000000000000000 ) ) ;
#6288=DIRECTION ( 'NONE',  ( 0.000000000000000000, -0.000000000000000000, -1.000000000000000000 ) ) ;
#6293=CARTESIAN_POINT ( 'NONE',  ( 6.190219624525621356, 0.4584813330253886265, -0.1849999999999999978 ) ) ;
#6294=ORIENTED_EDGE ( 'NONE', *, *, #5844, .T. ) ;
#6295=ORIENTED_EDGE ( 'NONE', *, *, #1316, .T. ) ;
#6298=EDGE_CURVE ( 'NONE', #2552, #7593, #6253, .T. ) ;
#6310=CARTESIAN_POINT ( 'NONE',  ( -0.02822771919328412663, 0.03615965030273324970, -0.1250000000000000000 ) ) ;
#6313=VERTEX_POINT ( 'NONE', #1918 ) ;
#6321=AXIS2_PLACEMENT_3D ( 'NONE', #5627, #1813, #3662 ) ;
#6323=CARTESIAN_POINT ( 'NONE',  ( 1.275565605498405253, -0.08258253728086821510, -0.1849999999999999978 ) ) ;
#6330=DIRECTION ( 'NONE',  ( -0.6568496200222107007, -0.7540216022612863389, 0.000000000000000000 ) ) ;
#6332=DIRECTION ( 'NONE',  ( -0.000000000000000000, 0.000000000000000000, -1.000000000000000000 ) ) ;
#6335=ORIENTED_EDGE ( 'NONE', *, *, #3991, .F. ) ;
#6336=AXIS2_PLACEMENT_3D ( 'NONE', #3721, #7570, #603 ) ;
#6344=CARTESIAN_POINT ( 'NONE',  ( -1.432604426929670938, 0.8194101287839820058, -0.1250000000000000000 ) ) ;
#6351=VECTOR ( 'NONE', #3521, 39.37007874015748143 ) ;
#6357=CARTESIAN_POINT ( 'NONE',  ( 3.666415866878781848, -8.185094079965441694, -0.1849999999999999978 ) ) ;
#6359=CARTESIAN_POINT ( 'NONE',  ( 1.258616367985684104, -0.02482036785324303815, -0.1849999999999999978 ) ) ;
#6366=AXIS2_PLACEMENT_3D ( 'NONE', #1959, #4465, #2045 ) ;
#6367=VECTOR ( 'NONE', #7386, 39.37007874015748854 ) ;
#6374=AXIS2_PLACEMENT_3D ( 'NONE', #1826, #3677, #5608 ) ;
#6376=EDGE_LOOP ( 'NONE', ( #2770, #3008, #5754 ) ) ;
#6377=CIRCLE ( 'NONE', #5070, 0.2499962251234248700 ) ;
#6380=PLANE ( 'NONE',  #4381 ) ;
#6385=VERTEX_POINT ( 'NONE', #6344 ) ;
#6387=ORIENTED_EDGE ( 'NONE', *, *, #6094, .F. ) ;
#6389=DIRECTION ( 'NONE',  ( 0.6568496200222107007, 0.7540216022612862279, -0.000000000000000000 ) ) ;
#6392=VERTEX_POINT ( 'NONE', #1989 ) ;
#6393=EDGE_CURVE ( 'NONE', #7842, #3224, #6275, .T. ) ;
#6394=FACE_OUTER_BOUND ( 'NONE', #1823, .T. ) ;
#6396=ORIENTED_EDGE ( 'NONE', *, *, #2521, .F. ) ;
#6397=EDGE_CURVE ( 'NONE', #5921, #5439, #3186, .T. ) ;
#6398=DIRECTION ( 'NONE',  ( 1.000000000000000000, 0.000000000000000000, 0.000000000000000000 ) ) ;
#6400=ADVANCED_FACE ( 'NONE', ( #3151 ), #67, .T. ) ;
#6417=DIRECTION ( 'NONE',  ( -0.000000000000000000, -0.000000000000000000, 1.000000000000000000 ) ) ;
#6421=DIRECTION ( 'NONE',  ( -0.000000000000000000, -0.000000000000000000, 1.000000000000000000 ) ) ;
#6422=FACE_OUTER_BOUND ( 'NONE', #6673, .T. ) ;
#6425=ORIENTED_EDGE ( 'NONE', *, *, #1319, .F. ) ;
#6433=CARTESIAN_POINT ( 'NONE',  ( -1.855136387357835481, 0.9645206712600612464, -0.08100000000000007194 ) ) ;
#6445=MANIFOLD_SOLID_BREP ( 'Fillet8', #7652 ) ;
#6446=AXIS2_PLACEMENT_3D ( 'NONE', #2643, #5897, #2037 ) ;
#6447=ORIENTED_EDGE ( 'NONE', *, *, #378, .T. ) ;
#6455=VECTOR ( 'NONE', #5375, 39.37007874015748143 ) ;
#6458=EDGE_LOOP ( 'NONE', ( #8065, #1409, #4071, #901, #1498 ) ) ;
#6460=VECTOR ( 'NONE', #5937, 39.37007874015748143 ) ;
#6465=LINE ( 'NONE', #5808, #7254 ) ;
#6466=FACE_OUTER_BOUND ( 'NONE', #3826, .T. ) ;
#6467=DIRECTION ( 'NONE',  ( -0.9987955914953421388, -0.04906492035527518225, 0.000000000000000000 ) ) ;
#6478=CARTESIAN_POINT ( 'NONE',  ( 3.666415866878781848, -8.185094079965441694, -0.1250000000000000000 ) ) ;
#6489=ADVANCED_FACE ( 'NONE', ( #6466 ), #7121, .F. ) ;
#6491=EDGE_CURVE ( 'NONE', #4303, #7230, #879, .T. ) ;
#6492=EDGE_CURVE ( 'NONE', #5845, #4303, #4940, .T. ) ;
#6494=EDGE_CURVE ( 'NONE', #7764, #4881, #7168, .T. ) ;
#6497=ORIENTED_EDGE ( 'NONE', *, *, #7986, .F. ) ;
#6500=DIRECTION ( 'NONE',  ( -0.000000000000000000, -0.000000000000000000, -1.000000000000000000 ) ) ;
#6503=LINE ( 'NONE', #2257, #8062 ) ;
#6506=EDGE_CURVE ( 'NONE', #7782, #6877, #1923, .T. ) ;
#6510=VECTOR ( 'NONE', #915, 39.37007874015748143 ) ;
#6515=ORIENTED_EDGE ( 'NONE', *, *, #3180, .F. ) ;
#6517=ORIENTED_EDGE ( 'NONE', *, *, #6181, .T. ) ;
#6519=AXIS2_PLACEMENT_3D ( 'NONE', #7412, #2400, #1098 ) ;
#6522=VECTOR ( 'NONE', #3099, 39.37007874015748143 ) ;
#6523=DIRECTION ( 'NONE',  ( 0.9987955914953421388, 0.04906492035527377366, 0.000000000000000000 ) ) ;
#6524=DIRECTION ( 'NONE',  ( -0.000000000000000000, -0.000000000000000000, -1.000000000000000000 ) ) ;
#6527=DIRECTION ( 'NONE',  ( 0.000000000000000000, -0.000000000000000000, -1.000000000000000000 ) ) ;
#6528=DIRECTION ( 'NONE',  ( -0.9987955914953421388, -0.04906492035527377366, 0.000000000000000000 ) ) ;
#6531=CYLINDRICAL_SURFACE ( 'NONE', #1653, 9.064497838702109789 ) ;
#6535=LINE ( 'NONE', #1638, #5996 ) ;
#6538=CYLINDRICAL_SURFACE ( 'NONE', #1644, 0.2149999999999995803 ) ;
#6543=EDGE_CURVE ( 'NONE', #4885, #1649, #233, .T. ) ;
#6545=DIRECTION ( 'NONE',  ( 0.04906492035527816598, -0.9987955914953420278, 0.000000000000000000 ) ) ;
#6550=ORIENTED_EDGE ( 'NONE', *, *, #1731, .T. ) ;
#6556=DIRECTION ( 'NONE',  ( -0.4964005096718474008, -0.8680936205257645533, 0.000000000000000000 ) ) ;
#6557=CARTESIAN_POINT ( 'NONE',  ( 1.472947776714219836, 0.7825821671288679671, 5.393636709996481038 ) ) ;
#6558=ADVANCED_FACE ( 'NONE', ( #5282 ), #1552, .T. ) ;
#6560=CARTESIAN_POINT ( 'NONE',  ( 1.475891671935536609, 0.7226544316391472211, 0.09375000000000005551 ) ) ;
#6564=CARTESIAN_POINT ( 'NONE',  ( 3.690413561029368683, -8.374393170229348371, 0.1849999999999999978 ) ) ;
#6569=ORIENTED_EDGE ( 'NONE', *, *, #5788, .T. ) ;
#6571=LINE ( 'NONE', #1604, #961 ) ;
#6582=ORIENTED_EDGE ( 'NONE', *, *, #1537, .T. ) ;
#6587=ADVANCED_FACE ( 'NONE', ( #311 ), #4086, .T. ) ;
#6588=DIRECTION ( 'NONE',  ( -1.000000000000000000, 0.000000000000000000, 0.000000000000000000 ) ) ;
#6589=EDGE_CURVE ( 'NONE', #81, #5187, #3729, .T. ) ;
#6616=VERTEX_POINT ( 'NONE', #2392 ) ;
#6620=ORIENTED_EDGE ( 'NONE', *, *, #2363, .F. ) ;
#6622=ORIENTED_EDGE ( 'NONE', *, *, #4390, .F. ) ;
#6626=CARTESIAN_POINT ( 'NONE',  ( 1.353790921086396093, 0.002306479836701611809, -0.1250000000000000278 ) ) ;
#6630=CARTESIAN_POINT ( 'NONE',  ( -1.424379639128854791, 0.8545203780043559849, -0.1657613293278376587 ) ) ;
#6633=VECTOR ( 'NONE', #6920, 39.37007874015748143 ) ;
#6635=LINE ( 'NONE', #5445, #6351 ) ;
#6636=DIRECTION ( 'NONE',  ( -0.000000000000000000, 0.000000000000000000, -1.000000000000000000 ) ) ;
#6640=DIRECTION ( 'NONE',  ( -1.000000000000000000, 0.000000000000000000, 0.000000000000000000 ) ) ;
#6642=EDGE_CURVE ( 'NONE', #5439, #5004, #6787, .T. ) ;
#6645=AXIS2_PLACEMENT_3D ( 'NONE', #5343, #4714, #6676 ) ;
#6649=ADVANCED_FACE ( 'NONE', ( #3055 ), #5477, .F. ) ;
#6665=CARTESIAN_POINT ( 'NONE',  ( 1.353816004522938599, 0.002313473902802895728, -0.1250000000000000278 ) ) ;
#6668=FACE_OUTER_BOUND ( 'NONE', #6904, .T. ) ;
#6673=EDGE_LOOP ( 'NONE', ( #5190, #5833, #4535, #1401 ) ) ;
#6676=DIRECTION ( 'NONE',  ( -1.000000000000000000, 0.000000000000000000, 0.000000000000000000 ) ) ;
#6679=DIRECTION ( 'NONE',  ( -0.6568496200222107007, -0.7540216022612862279, 0.000000000000000000 ) ) ;
#6684=ADVANCED_FACE ( 'NONE', ( #3017 ), #1206, .F. ) ;
#6686=ORIENTED_EDGE ( 'NONE', *, *, #2235, .T. ) ;
#6693=EDGE_CURVE ( 'NONE', #5116, #963, #1796, .T. ) ;
#6698=VERTEX_POINT ( 'NONE', #1787 ) ;
#6705=CYLINDRICAL_SURFACE ( 'NONE', #4290, 0.1250000000000000000 ) ;
#6712=CIRCLE ( 'NONE', #7103, 8.573908398499121120 ) ;
#6717=DIRECTION ( 'NONE',  ( 1.000000000000000000, 0.000000000000000000, 0.000000000000000000 ) ) ;
#6724=DIRECTION ( 'NONE',  ( -1.000000000000000000, 0.000000000000000000, 0.000000000000000000 ) ) ;
#6726=ORIENTED_EDGE ( 'NONE', *, *, #6492, .F. ) ;
#6729=LINE ( 'NONE', #6773, #5008 ) ;
#6740=VERTEX_POINT ( 'NONE', #6223 ) ;
#6741=ORIENTED_EDGE ( 'NONE', *, *, #4091, .T. ) ;
#6743=ADVANCED_FACE ( 'NONE', ( #3103 ), #6705, .F. ) ;
#6754=CARTESIAN_POINT ( 'NONE',  ( -1.855136387357835481, 0.9645206712600612464, -0.08100000000000007194 ) ) ;
#6758=CARTESIAN_POINT ( 'NONE',  ( 6.185915932928153005, 0.4597367884986193753, -0.1250000000000000278 ) ) ;
#6764=VECTOR ( 'NONE', #6528, 39.37007874015748854 ) ;
#6771=AXIS2_PLACEMENT_3D ( 'NONE', #3265, #1298, #3807 ) ;
#6773=CARTESIAN_POINT ( 'NONE',  ( 3.221700243049673507, 0.8684880333666036289, 5.393636709996481038 ) ) ;
#6778=DIRECTION ( 'NONE',  ( -0.7498009116086186143, 0.6531728565937872100, 0.1056589435873571958 ) ) ;
#6779=DIRECTION ( 'NONE',  ( -1.000000000000000000, 0.000000000000000000, 0.000000000000000000 ) ) ;
#6780=ORIENTED_EDGE ( 'NONE', *, *, #1690, .T. ) ;
#6784=LINE ( 'NONE', #4826, #6522 ) ;
#6787=LINE ( 'NONE', #7921, #7931 ) ;
#6790=DIRECTION ( 'NONE',  ( -0.000000000000000000, 0.000000000000000000, 1.000000000000000000 ) ) ;
#6798=CARTESIAN_POINT ( 'NONE',  ( 6.067386035484801710, 0.2407470087491039856, -0.1250000000000000000 ) ) ;
#6802=DIRECTION ( 'NONE',  ( 0.7540216022612858948, -0.6568496200222110337, 0.000000000000000000 ) ) ;
#6807=EDGE_CURVE ( 'NONE', #796, #6698, #6377, .T. ) ;
#6808=CARTESIAN_POINT ( 'NONE',  ( 3.566133519791359507, 0.3212125039962131501, 0.1850000000000003586 ) ) ;
#6811=VERTEX_POINT ( 'NONE', #1863 ) ;
#6812=EDGE_LOOP ( 'NONE', ( #3369, #2014, #5877, #3577, #1768 ) ) ;
#6813=CARTESIAN_POINT ( 'NONE',  ( 6.067840808230170246, 0.2405569712445295161, -0.1849999999999999978 ) ) ;
#6819=DIRECTION ( 'NONE',  ( -0.7540216022612862279, 0.6568496200222107007, 0.000000000000000000 ) ) ;
#6822=DIRECTION ( 'NONE',  ( 0.7540216022612862279, -0.6568496200222107007, 0.000000000000000000 ) ) ;
#6824=EDGE_LOOP ( 'NONE', ( #6515, #6294, #7888, #3517, #6582 ) ) ;
#6826=DIRECTION ( 'NONE',  ( 1.000000000000000000, 0.000000000000000000, 0.000000000000000000 ) ) ;
#6827=CARTESIAN_POINT ( 'NONE',  ( 6.067840808230170246, 0.2405569712445295161, -0.1849999999999999978 ) ) ;
#6828=ADVANCED_FACE ( 'NONE', ( #4486 ), #3219, .T. ) ;
#6829=EDGE_CURVE ( 'NONE', #1614, #2946, #17, .T. ) ;
#6833=ORIENTED_EDGE ( 'NONE', *, *, #7002, .T. ) ;
#6836=VECTOR ( 'NONE', #235, 39.37007874015748143 ) ;
#6840=EDGE_CURVE ( 'NONE', #761, #2895, #1293, .T. ) ;
#6841=DIRECTION ( 'NONE',  ( 0.000000000000000000, 0.000000000000000000, -1.000000000000000000 ) ) ;
#6842=FACE_OUTER_BOUND ( 'NONE', #3252, .T. ) ;
#6845=EDGE_CURVE ( 'NONE', #7112, #774, #5135, .T. ) ;
#6848=CARTESIAN_POINT ( 'NONE',  ( 6.190221022838899856, 0.4584861219976859026, 5.393636709996481038 ) ) ;
#6852=LINE ( 'NONE', #4890, #210 ) ;
#6856=VERTEX_POINT ( 'NONE', #6914 ) ;
#6857=AXIS2_PLACEMENT_3D ( 'NONE', #7645, #7039, #1415 ) ;
#6860=DIRECTION ( 'NONE',  ( -1.000000000000000000, 0.000000000000000000, 0.000000000000000000 ) ) ;
#6863=DIRECTION ( 'NONE',  ( 0.000000000000000000, -0.000000000000000000, -1.000000000000000000 ) ) ;
#6870=AXIS2_PLACEMENT_3D ( 'NONE', #4701, #974, #1049 ) ;
#6872=AXIS2_PLACEMENT_3D ( 'NONE', #983, #7246, #4133 ) ;
#6876=DIRECTION ( 'NONE',  ( 0.000000000000000000, 0.000000000000000000, -1.000000000000000000 ) ) ;
#6877=VERTEX_POINT ( 'NONE', #57 ) ;
#6884=PLANE ( 'NONE',  #6269 ) ;
#6885=AXIS2_PLACEMENT_3D ( 'NONE', #5745, #660, #3 ) ;
#6887=ORIENTED_EDGE ( 'NONE', *, *, #1577, .F. ) ;
#6891=VECTOR ( 'NONE', #4709, 39.37007874015748143 ) ;
#6893=AXIS2_PLACEMENT_3D ( 'NONE', #1850, #7988, #6898 ) ;
#6895=ORIENTED_EDGE ( 'NONE', *, *, #5052, .F. ) ;
#6898=DIRECTION ( 'NONE',  ( 1.000000000000000000, 0.000000000000000000, 0.000000000000000000 ) ) ;
#6903=EDGE_CURVE ( 'NONE', #7381, #4068, #5464, .T. ) ;
#6904=EDGE_LOOP ( 'NONE', ( #1332, #6234, #4999, #5509, #1933, #1082, #5352, #7707, #7430 ) ) ;
#6905=VECTOR ( 'NONE', #6679, 39.37007874015748143 ) ;
#6914=CARTESIAN_POINT ( 'NONE',  ( 1.258671604940864608, -0.02501003737716508274, -0.1849999999999999978 ) ) ;
#6918=ORIENTED_EDGE ( 'NONE', *, *, #4786, .T. ) ;
#6920=DIRECTION ( 'NONE',  ( 0.8680936205257663296, -0.4964005096718443477, 0.000000000000000000 ) ) ;
#6922=CARTESIAN_POINT ( 'NONE',  ( -1.420319797626316216, 0.8334728170008732784, 0.1249999999999995559 ) ) ;
#6928=ORIENTED_EDGE ( 'NONE', *, *, #634, .F. ) ;
#6930=DIRECTION ( 'NONE',  ( -1.000000000000000000, 0.000000000000000000, 0.000000000000000000 ) ) ;
#6932=CARTESIAN_POINT ( 'NONE',  ( 1.466665248995881354, 0.6909135088951505743, 0.1250000000000000000 ) ) ;
#6942=EDGE_CURVE ( 'NONE', #3224, #2946, #1147, .T. ) ;
#6946=( NAMED_UNIT ( * ) SI_UNIT ( $, .STERADIAN. ) SOLID_ANGLE_UNIT ( ) );
#6949=DIRECTION ( 'NONE',  ( 1.000000000000000000, 0.000000000000000000, 0.000000000000000000 ) ) ;
#6956=DIRECTION ( 'NONE',  ( -0.000000000000000000, -0.000000000000000000, -1.000000000000000000 ) ) ;
#6958=CARTESIAN_POINT ( 'NONE',  ( -1.484384414703910027, 0.9067922411947360040, 0.1720737575213688586 ) ) ;
#6961=CYLINDRICAL_SURFACE ( 'NONE', #2413, 0.2149999999999995803 ) ;
#6963=DIRECTION ( 'NONE',  ( 0.6568496200222107007, 0.7540216022612862279, -0.000000000000000000 ) ) ;
#6968=VECTOR ( 'NONE', #6876, 39.37007874015748143 ) ;
#6970=CARTESIAN_POINT ( 'NONE',  ( 5.983714301115757195, -0.05774751952986827835, 0.1850000000000003586 ) ) ;
#6977=VECTOR ( 'NONE', #1104, 39.37007874015748143 ) ;
#6980=EDGE_LOOP ( 'NONE', ( #1262, #1617, #6396, #3226 ) ) ;
#6981=DIRECTION ( 'NONE',  ( 0.000000000000000000, 0.000000000000000000, 1.000000000000000000 ) ) ;
#6985=CARTESIAN_POINT ( 'NONE',  ( 6.067385397437120353, 0.2407432673787524013, -0.1849999999999999978 ) ) ;
#6996=CARTESIAN_POINT ( 'NONE',  ( 1.472947776714219836, 0.7825821671288679671, -0.1849999999999999978 ) ) ;
#7002=EDGE_CURVE ( 'NONE', #713, #6811, #4605, .T. ) ;
#7003=CARTESIAN_POINT ( 'NONE',  ( 3.672798492683009286, -8.252032378159654513, 5.393636709996481038 ) ) ;
#7006=PLANE ( 'NONE',  #2565 ) ;
#7008=ORIENTED_EDGE ( 'NONE', *, *, #2374, .T. ) ;
#7038=ORIENTED_EDGE ( 'NONE', *, *, #3187, .T. ) ;
#7039=DIRECTION ( 'NONE',  ( 0.6568496200222107007, 0.7540216022612863389, -0.000000000000000000 ) ) ;
#7046=ORIENTED_EDGE ( 'NONE', *, *, #1835, .F. ) ;
#7048=CARTESIAN_POINT ( 'NONE',  ( 6.067840808230170246, 0.2405569712445295161, -0.1250000000000004441 ) ) ;
#7052=DIRECTION ( 'NONE',  ( 0.9968059542140783602, 0.000000000000000000, 0.07986169071188227442 ) ) ;
#7053=LINE ( 'NONE', #7739, #3487 ) ;
#7054=ORIENTED_EDGE ( 'NONE', *, *, #6298, .T. ) ;
#7055=CARTESIAN_POINT ( 'NONE',  ( -1.723766588794375387, 1.115324847714046497, -0.08100000000000007194 ) ) ;
#7068=ORIENTED_EDGE ( 'NONE', *, *, #2528, .F. ) ;
#7069=ORIENTED_EDGE ( 'NONE', *, *, #1319, .T. ) ;
#7072=LINE ( 'NONE', #1413, #4115 ) ;
#7076=LINE ( 'NONE', #2078, #3953 ) ;
#7078=EDGE_CURVE ( 'NONE', #7153, #375, #177, .T. ) ;
#7084=LINE ( 'NONE', #2174, #6510 ) ;
#7085=EDGE_CURVE ( 'NONE', #5716, #4569, #2068, .T. ) ;
#7088=LINE ( 'NONE', #4031, #6455 ) ;
#7090=EDGE_CURVE ( 'NONE', #1621, #658, #6503, .T. ) ;
#7093=CARTESIAN_POINT ( 'NONE',  ( 1.475891671935536609, 0.7226544316391472211, 0.09375000000000005551 ) ) ;
#7096=EDGE_LOOP ( 'NONE', ( #2878, #3105, #3483, #5719, #5465, #1103, #2108, #551 ) ) ;
#7101=ADVANCED_FACE ( 'NONE', ( #6200 ), #7424, .T. ) ;
#7103=AXIS2_PLACEMENT_3D ( 'NONE', #5050, #4511, #6398 ) ;
#7106=CARTESIAN_POINT ( 'NONE',  ( 1.475891671935536609, 0.7226544316391472211, 5.393636709996481038 ) ) ;
#7110=AXIS2_PLACEMENT_3D ( 'NONE', #7855, #1592, #6640 ) ;
#7111=ORIENTED_EDGE ( 'NONE', *, *, #6033, .T. ) ;
#7112=VERTEX_POINT ( 'NONE', #4437 ) ;
#7117=ORIENTED_EDGE ( 'NONE', *, *, #670, .T. ) ;
#7120=CARTESIAN_POINT ( 'NONE',  ( 3.221700243049672174, 0.8684880333666047392, 5.393636709996481038 ) ) ;
#7121=PLANE ( 'NONE',  #4931 ) ;
#7122=FACE_OUTER_BOUND ( 'NONE', #5280, .T. ) ;
#7126=CARTESIAN_POINT ( 'NONE',  ( 3.672767464462126430, -8.314346814944791220, -0.1849999999999999978 ) ) ;
#7132=DIRECTION ( 'NONE',  ( -0.07966912593697374201, 0.06940203694730361084, 0.9944024274105548455 ) ) ;
#7133=DIRECTION ( 'NONE',  ( 0.7498009116086189474, -0.6531728565937869879, 0.1056589435873569599 ) ) ;
#7135=FACE_OUTER_BOUND ( 'NONE', #5166, .T. ) ;
#7142=AXIS2_PLACEMENT_3D ( 'NONE', #4955, #4332, #686 ) ;
#7148=CIRCLE ( 'NONE', #3750, 9.004497838701050583 ) ;
#7153=VERTEX_POINT ( 'NONE', #2410 ) ;
#7157=LINE ( 'NONE', #6012, #4007 ) ;
#7158=CIRCLE ( 'NONE', #1129, 0.4999999999999997224 ) ;
#7164=ORIENTED_EDGE ( 'NONE', *, *, #993, .F. ) ;
#7167=VERTEX_POINT ( 'NONE', #4350 ) ;
#7168=CIRCLE ( 'NONE', #4675, 0.1250000000000001110 ) ;
#7175=DIRECTION ( 'NONE',  ( 1.000000000000000000, -2.283006407345790279E-13, 0.000000000000000000 ) ) ;
#7176=FACE_OUTER_BOUND ( 'NONE', #7472, .T. ) ;
#7186=DIRECTION ( 'NONE',  ( -0.000000000000000000, 0.000000000000000000, 1.000000000000000000 ) ) ;
#7188=ORIENTED_EDGE ( 'NONE', *, *, #578, .F. ) ;
#7196=DIRECTION ( 'NONE',  ( -0.7498009116086186143, 0.6531728565937872100, 0.1056589435873571958 ) ) ;
#7203=CYLINDRICAL_SURFACE ( 'NONE', #3703, 8.573908398499121120 ) ;
#7207=DIRECTION ( 'NONE',  ( -1.000000000000000000, 0.000000000000000000, 0.000000000000000000 ) ) ;
#7209=ORIENTED_EDGE ( 'NONE', *, *, #4989, .T. ) ;
#7210=CARTESIAN_POINT ( 'NONE',  ( 1.466665248995881576, 0.6909135088951512405, -0.1250000000000000000 ) ) ;
#7215=ORIENTED_EDGE ( 'NONE', *, *, #6642, .F. ) ;
#7216=CARTESIAN_POINT ( 'NONE',  ( -1.723766588794375387, 1.115324847714046497, -0.08100000000000007194 ) ) ;
#7218=ORIENTED_EDGE ( 'NONE', *, *, #5839, .F. ) ;
#7227=EDGE_LOOP ( 'NONE', ( #4727, #5981, #6113, #4015 ) ) ;
#7229=AXIS2_PLACEMENT_3D ( 'NONE', #1828, #1398, #4329 ) ;
#7230=VERTEX_POINT ( 'NONE', #8061 ) ;
#7237=DIRECTION ( 'NONE',  ( 0.000000000000000000, -0.000000000000000000, 1.000000000000000000 ) ) ;
#7241=FACE_OUTER_BOUND ( 'NONE', #5959, .T. ) ;
#7246=DIRECTION ( 'NONE',  ( 0.000000000000000000, -0.000000000000000000, -1.000000000000000000 ) ) ;
#7250=AXIS2_PLACEMENT_3D ( 'NONE', #7106, #2196, #6545 ) ;
#7254=VECTOR ( 'NONE', #7726, 39.37007874015748854 ) ;
#7266=ORIENTED_EDGE ( 'NONE', *, *, #1836, .F. ) ;
#7267=AXIS2_PLACEMENT_3D ( 'NONE', #3061, #8048, #6826 ) ;
#7268=ORIENTED_EDGE ( 'NONE', *, *, #6257, .F. ) ;
#7274=CARTESIAN_POINT ( 'NONE',  ( -1.803041671366327314, 1.104810305277056592, 0.1649762307749162715 ) ) ;
#7276=DESIGN_CONTEXT ( 'detailed design', #1541, 'design' ) ;
#7279=DIRECTION ( 'NONE',  ( -0.000000000000000000, -0.000000000000000000, -1.000000000000000000 ) ) ;
#7288=AXIS2_PLACEMENT_3D ( 'NONE', #850, #4703, #268 ) ;
#7301=AXIS2_PLACEMENT_3D ( 'NONE', #245, #4553, #4586 ) ;
#7304=DIRECTION ( 'NONE',  ( -0.000000000000000000, -0.000000000000000000, 1.000000000000000000 ) ) ;
#7308=CARTESIAN_POINT ( 'NONE',  ( 5.999999999999997335, -1.164450207299392140E-14, -0.1849999999999999978 ) ) ;
#7326=( BOUNDED_CURVE ( )  B_SPLINE_CURVE ( 3, ( #2568, #6922, #5148, #5736 ),
 .UNSPECIFIED., .F., .F. ) 
 B_SPLINE_CURVE_WITH_KNOTS ( ( 4, 4 ),
 ( 4.712388980384713655, 6.283185307179586232 ),
 .UNSPECIFIED. ) 
 CURVE ( )  GEOMETRIC_REPRESENTATION_ITEM ( )  RATIONAL_B_SPLINE_CURVE ( ( 1.000000000000000000, 0.8047378541243705996, 0.8047378541243705996, 1.000000000000000000 ) ) 
 REPRESENTATION_ITEM ( '' )  );
#7329=DIRECTION ( 'NONE',  ( -0.000000000000000000, 0.000000000000000000, 1.000000000000000000 ) ) ;
#7333=LINE ( 'NONE', #2951, #2942 ) ;
#7334=DIRECTION ( 'NONE',  ( -0.6568496200222107007, -0.7540216022612863389, 0.000000000000000000 ) ) ;
#7336=ORIENTED_EDGE ( 'NONE', *, *, #5550, .T. ) ;
#7337=DIRECTION ( 'NONE',  ( -0.000000000000000000, -0.000000000000000000, 1.000000000000000000 ) ) ;
#7340=DIRECTION ( 'NONE',  ( -1.000000000000000000, 0.000000000000000000, 0.000000000000000000 ) ) ;
#7341=ADVANCED_FACE ( 'NONE', ( #2699 ), #5867, .T. ) ;
#7362=VECTOR ( 'NONE', #7771, 39.37007874015748143 ) ;
#7366=AXIS2_PLACEMENT_3D ( 'NONE', #1892, #7382, #1157 ) ;
#7371=AXIS2_PLACEMENT_3D ( 'NONE', #3118, #1183, #4960 ) ;
#7381=VERTEX_POINT ( 'NONE', #3973 ) ;
#7382=DIRECTION ( 'NONE',  ( 0.4964005096718443477, 0.8680936205257663296, -0.000000000000000000 ) ) ;
#7386=DIRECTION ( 'NONE',  ( -0.2815666759589948720, 0.9595416650617117904, -0.000000000000000000 ) ) ;
#7392=ADVANCED_FACE ( 'NONE', ( #6394 ), #775, .F. ) ;
#7396=AXIS2_PLACEMENT_3D ( 'NONE', #7048, #6527, #7175 ) ;
#7397=EDGE_CURVE ( 'NONE', #4782, #4126, #1256, .T. ) ;
#7409=LINE ( 'NONE', #3681, #1488 ) ;
#7412=CARTESIAN_POINT ( 'NONE',  ( -1.723766588794375609, 1.115324847714047385, -0.08100000000000007194 ) ) ;
#7413=CARTESIAN_POINT ( 'NONE',  ( 6.068104892000603101, -0.009251957739379085624, 0.1250000000000000000 ) ) ;
#7416=EDGE_LOOP ( 'NONE', ( #2494, #2107, #6620, #7188, #3004, #3153, #6686, #6172 ) ) ;
#7424=PLANE ( 'NONE',  #1657 ) ;
#7428=FACE_OUTER_BOUND ( 'NONE', #2247, .T. ) ;
#7429=AXIS2_PLACEMENT_3D ( 'NONE', #1111, #1719, #5230 ) ;
#7430=ORIENTED_EDGE ( 'NONE', *, *, #1366, .T. ) ;
#7431=VECTOR ( 'NONE', #6071, 39.37007874015748143 ) ;
#7433=FACE_OUTER_BOUND ( 'NONE', #7923, .T. ) ;
#7435=LINE ( 'NONE', #4283, #3191 ) ;
#7439=EDGE_CURVE ( 'NONE', #713, #2155, #7084, .T. ) ;
#7442=DIRECTION ( 'NONE',  ( -0.000000000000000000, -0.000000000000000000, 1.000000000000000000 ) ) ;
#7445=DIRECTION ( 'NONE',  ( -1.000000000000000000, 0.000000000000000000, 0.000000000000000000 ) ) ;
#7447=DIRECTION ( 'NONE',  ( -1.000000000000000000, 0.000000000000000000, 0.000000000000000000 ) ) ;
#7452=ORIENTED_EDGE ( 'NONE', *, *, #7974, .F. ) ;
#7455=DIRECTION ( 'NONE',  ( 0.000000000000000000, -0.000000000000000000, -1.000000000000000000 ) ) ;
#7459=EDGE_CURVE ( 'NONE', #3415, #5374, #6852, .T. ) ;
#7463=ORIENTED_EDGE ( 'NONE', *, *, #4747, .F. ) ;
#7469=FACE_OUTER_BOUND ( 'NONE', #1605, .T. ) ;
#7472=EDGE_LOOP ( 'NONE', ( #3047, #106, #4462, #4875 ) ) ;
#7473=ORIENTED_EDGE ( 'NONE', *, *, #7459, .F. ) ;
#7475=CARTESIAN_POINT ( 'NONE',  ( 3.659299226295303686, -8.245510427152350275, -0.1250000000000004441 ) ) ;
#7477=CARTESIAN_POINT ( 'NONE',  ( -0.9157629057885486867, 0.6051665869063995729, 0.1250000000000000000 ) ) ;
#7481=EDGE_CURVE ( 'NONE', #340, #8047, #2304, .T. ) ;
#7482=ORIENTED_EDGE ( 'NONE', *, *, #2680, .F. ) ;
#7485=AXIS2_PLACEMENT_3D ( 'NONE', #359, #3402, #2769 ) ;
#7488=CARTESIAN_POINT ( 'NONE',  ( 1.475891671935536609, 0.7226544316391472211, 5.393636709996481038 ) ) ;
#7491=ADVANCED_FACE ( 'NONE', ( #2544 ), #2462, .F. ) ;
#7496=EDGE_CURVE ( 'NONE', #4174, #3224, #2185, .T. ) ;
#7498=CARTESIAN_POINT ( 'NONE',  ( 1.258616367985684104, -0.02482036785324303815, 0.1849999999999999978 ) ) ;
#7500=ORIENTED_EDGE ( 'NONE', *, *, #1836, .T. ) ;
#7507=ORIENTED_EDGE ( 'NONE', *, *, #3344, .F. ) ;
#7508=DIRECTION ( 'NONE',  ( 1.000000000000000000, 0.000000000000000000, 0.000000000000000000 ) ) ;
#7516=ORIENTED_EDGE ( 'NONE', *, *, #670, .F. ) ;
#7522=ORIENTED_EDGE ( 'NONE', *, *, #1472, .F. ) ;
#7528=CIRCLE ( 'NONE', #6872, 8.633956053943499853 ) ;
#7537=EDGE_CURVE ( 'NONE', #3622, #6856, #1239, .T. ) ;
#7546=AXIS2_PLACEMENT_3D ( 'NONE', #5251, #3522, #2284 ) ;
#7549=VECTOR ( 'NONE', #2707, 39.37007874015748143 ) ;
#7550=EDGE_CURVE ( 'NONE', #297, #7167, #8056, .T. ) ;
#7551=ADVANCED_FACE ( 'NONE', ( #7433 ), #5188, .T. ) ;
#7554=CARTESIAN_POINT ( 'NONE',  ( 3.690413561029368683, -8.374393170229348371, 0.1849999999999999978 ) ) ;
#7570=DIRECTION ( 'NONE',  ( -0.000000000000000000, -0.000000000000000000, -1.000000000000000000 ) ) ;
#7581=CARTESIAN_POINT ( 'NONE',  ( 1.356840083662244734, 0.003162463486408387866, 0.1850000000000003586 ) ) ;
#7591=EDGE_CURVE ( 'NONE', #898, #6392, #2693, .T. ) ;
#7593=VERTEX_POINT ( 'NONE', #1310 ) ;
#7599=DIRECTION ( 'NONE',  ( -0.000000000000000000, -0.000000000000000000, 1.000000000000000000 ) ) ;
#7603=ORIENTED_EDGE ( 'NONE', *, *, #1879, .T. ) ;
#7616=ORIENTED_EDGE ( 'NONE', *, *, #7002, .F. ) ;
#7618=CARTESIAN_POINT ( 'NONE',  ( -0.1250000000000000000, 0.000000000000000000, 0.1250000000000000000 ) ) ;
#7622=CARTESIAN_POINT ( 'NONE',  ( -1.424379639128854791, 0.8545203780043559849, -0.1657613293278376587 ) ) ;
#7623=FACE_OUTER_BOUND ( 'NONE', #271, .T. ) ;
#7627=ORIENTED_EDGE ( 'NONE', *, *, #2423, .T. ) ;
#7631=CIRCLE ( 'NONE', #564, 8.513908398499120622 ) ;
#7638=AXIS2_PLACEMENT_3D ( 'NONE', #1442, #2066, #3870 ) ;
#7645=CARTESIAN_POINT ( 'NONE',  ( -1.855136387357835481, 0.9645206712600612464, -0.08100000000000007194 ) ) ;
#7652=CLOSED_SHELL ( 'NONE', ( #1678, #2885, #3997, #2572, #319, #633, #2790, #2830, #5092, #3391, #1685, #2189, #5246, #5887, #6743, #4794, #7341, #1181, #7491, #1178, #5647, #2121, #6489, #3748, #4049, #3068, #4491, #2884, #6684, #1325, #5700, #1783, #1971, #5636, #4041, #6106, #4852, #3246, #6649, #6400, #1417, #6558, #1725, #7551, #5827 ) ) ;
#7653=VECTOR ( 'NONE', #556, 39.37007874015748143 ) ;
#7655=CARTESIAN_POINT ( 'NONE',  ( -1.484384414703910027, 0.9067922411947358929, 0.1720737575213687476 ) ) ;
#7661=CIRCLE ( 'NONE', #5176, 8.633956053943499853 ) ;
#7670=AXIS2_PLACEMENT_3D ( 'NONE', #36, #735, #3236 ) ;
#7677=CARTESIAN_POINT ( 'NONE',  ( 3.566133519791359507, 0.3212125039962120954, 0.1250000000000000278 ) ) ;
#7692=ORIENTED_EDGE ( 'NONE', *, *, #7550, .F. ) ;
#7700=PLANE ( 'NONE',  #3435 ) ;
#7707=ORIENTED_EDGE ( 'NONE', *, *, #2330, .T. ) ;
#7710=ORIENTED_EDGE ( 'NONE', *, *, #6250, .T. ) ;
#7714=EDGE_LOOP ( 'NONE', ( #6171, #6279, #4610, #5961 ) ) ;
#7715=DIRECTION ( 'NONE',  ( -0.6568496200222107007, -0.7540216022612862279, 0.000000000000000000 ) ) ;
#7716=PLANE ( 'NONE',  #694 ) ;
#7726=DIRECTION ( 'NONE',  ( -0.7540216022612861169, 0.6568496200222107007, 0.000000000000000000 ) ) ;
#7727=CARTESIAN_POINT ( 'NONE',  ( 1.258616367985684104, -0.02482036785324303815, -0.1849999999999999978 ) ) ;
#7733=LINE ( 'NONE', #4061, #6764 ) ;
#7736=DIRECTION ( 'NONE',  ( 0.7540216022612861169, -0.6568496200222109227, 0.000000000000000000 ) ) ;
#7739=CARTESIAN_POINT ( 'NONE',  ( 6.000000000000000888, 0.000000000000000000, 0.1250000000000000000 ) ) ;
#7753=CARTESIAN_POINT ( 'NONE',  ( 1.321981203096655788, -0.006563399200562533738, -0.1250000000000000278 ) ) ;
#7761=CARTESIAN_POINT ( 'NONE',  ( 6.191327929239392347, 0.4578608198540764507, 0.000000000000000000 ) ) ;
#7763=VECTOR ( 'NONE', #4633, 39.37007874015748143 ) ;
#7764=VERTEX_POINT ( 'NONE', #3376 ) ;
#7771=DIRECTION ( 'NONE',  ( -0.000000000000000000, -0.000000000000000000, -1.000000000000000000 ) ) ;
#7772=CIRCLE ( 'NONE', #4245, 0.2499999999999986955 ) ;
#7777=AXIS2_PLACEMENT_3D ( 'NONE', #4204, #8077, #5474 ) ;
#7779=CYLINDRICAL_SURFACE ( 'NONE', #3361, 9.124497838702110286 ) ;
#7781=CARTESIAN_POINT ( 'NONE',  ( 6.067385397437120353, 0.2407432673787524013, -0.1250000000000000000 ) ) ;
#7782=VERTEX_POINT ( 'NONE', #820 ) ;
#7785=EDGE_CURVE ( 'NONE', #5686, #1539, #5259, .T. ) ;
#7789=CIRCLE ( 'NONE', #1912, 8.696493751522730520 ) ;
#7802=CARTESIAN_POINT ( 'NONE',  ( -1.855136387357835481, 0.9645206712600612464, -0.2959999999999997078 ) ) ;
#7807=AXIS2_PLACEMENT_3D ( 'NONE', #44, #628, #1937 ) ;
#7811=CARTESIAN_POINT ( 'NONE',  ( -0.9142296270274463676, 0.5739542246721696106, 0.09374999999999998612 ) ) ;
#7815=VECTOR ( 'NONE', #4419, 39.37007874015748854 ) ;
#7819=DIRECTION ( 'NONE',  ( 1.000000000000000000, 0.000000000000000000, 0.000000000000000000 ) ) ;
#7822=DIRECTION ( 'NONE',  ( 0.000000000000000000, -0.000000000000000000, 1.000000000000000000 ) ) ;
#7827=EDGE_CURVE ( 'NONE', #4569, #5116, #605, .T. ) ;
#7830=ORIENTED_EDGE ( 'NONE', *, *, #2521, .T. ) ;
#7841=EDGE_CURVE ( 'NONE', #7230, #502, #6784, .T. ) ;
#7842=VERTEX_POINT ( 'NONE', #472 ) ;
#7848=CARTESIAN_POINT ( 'NONE',  ( -1.410683006424825692, 0.8425888524880515984, 0.2499905547878000789 ) ) ;
#7850=ORIENTED_EDGE ( 'NONE', *, *, #1978, .T. ) ;
#7852=CARTESIAN_POINT ( 'NONE',  ( -1.332203854133312548, 0.7742234353597469143, -0.1918577977169502180 ) ) ;
#7855=CARTESIAN_POINT ( 'NONE',  ( 6.067840808230170246, 0.2405569712445295161, 0.1850000000000003586 ) ) ;
#7859=ORIENTED_EDGE ( 'NONE', *, *, #7439, .T. ) ;
#7874=ORIENTED_EDGE ( 'NONE', *, *, #1039, .T. ) ;
#7877=VECTOR ( 'NONE', #3904, 39.37007874015748854 ) ;
#7880=DIRECTION ( 'NONE',  ( 0.6568496200222107007, 0.7540216022612862279, 0.000000000000000000 ) ) ;
#7882=ORIENTED_EDGE ( 'NONE', *, *, #7090, .T. ) ;
#7883=CYLINDRICAL_SURFACE ( 'NONE', #5274, 0.1249999999999998473 ) ;
#7885=LINE ( 'NONE', #517, #5023 ) ;
#7888=ORIENTED_EDGE ( 'NONE', *, *, #5248, .T. ) ;
#7897=DIRECTION ( 'NONE',  ( -0.9987955914953421388, -0.04906492035527377366, 0.000000000000000000 ) ) ;
#7901=DIRECTION ( 'NONE',  ( 0.6568496200222107007, 0.7540216022612862279, -0.000000000000000000 ) ) ;
#7908=ORIENTED_EDGE ( 'NONE', *, *, #6156, .F. ) ;
#7915=DIRECTION ( 'NONE',  ( 0.8680936205257663296, -0.4964005096718443477, 0.000000000000000000 ) ) ;
#7919=CYLINDRICAL_SURFACE ( 'NONE', #4634, 8.633956053943499853 ) ;
#7921=CARTESIAN_POINT ( 'NONE',  ( 4.013019369095008670, -4.147396371033809537, -0.1250000000000000000 ) ) ;
#7923=EDGE_LOOP ( 'NONE', ( #2332, #2670, #1209, #1530 ) ) ;
#7928=EDGE_CURVE ( 'NONE', #4493, #4174, #745, .T. ) ;
#7931=VECTOR ( 'NONE', #6822, 39.37007874015748143 ) ;
#7932=AXIS2_PLACEMENT_3D ( 'NONE', #3013, #591, #5512 ) ;
#7934=CARTESIAN_POINT ( 'NONE',  ( 1.472069962421740819, 0.7095069109563471033, 0.1250000000000000000 ) ) ;
#7938=EDGE_CURVE ( 'NONE', #502, #4907, #4205, .T. ) ;
#7943=ADVANCED_FACE ( 'NONE', ( #4977 ), #7998, .F. ) ;
#7944=CARTESIAN_POINT ( 'NONE',  ( 6.317381622560545473, 0.2407432673787524013, -0.1250000000000000000 ) ) ;
#7945=DIRECTION ( 'NONE',  ( -0.000000000000000000, -0.000000000000000000, -1.000000000000000000 ) ) ;
#7947=ORIENTED_EDGE ( 'NONE', *, *, #1080, .T. ) ;
#7958=PLANE ( 'NONE',  #2822 ) ;
#7969=ORIENTED_EDGE ( 'NONE', *, *, #2144, .T. ) ;
#7973=LINE ( 'NONE', #2403, #6977 ) ;
#7974=EDGE_CURVE ( 'NONE', #4612, #7782, #5728, .T. ) ;
#7984=CARTESIAN_POINT ( 'NONE',  ( -1.983451234524918227, 1.341543513548240529, -0.2959999999999997078 ) ) ;
#7986=EDGE_CURVE ( 'NONE', #5374, #813, #680, .T. ) ;
#7988=DIRECTION ( 'NONE',  ( -0.000000000000000000, 0.000000000000000000, 1.000000000000000000 ) ) ;
#7997=CARTESIAN_POINT ( 'NONE',  ( 6.067385397437120353, 0.2407432673787524013, -0.1849999999999999978 ) ) ;
#7998=CYLINDRICAL_SURFACE ( 'NONE', #7932, 0.2515937209583817280 ) ;
#7999=CARTESIAN_POINT ( 'NONE',  ( 6.000000000000001776, 0.000000000000000000, 0.1850000000000003586 ) ) ;
#8001=DIRECTION ( 'NONE',  ( 0.000000000000000000, 0.000000000000000000, -1.000000000000000000 ) ) ;
#8003=CIRCLE ( 'NONE', #2902, 0.2499999999999998057 ) ;
#8007=CARTESIAN_POINT ( 'NONE',  ( 2.056298385200680201, 0.7198786976815837457, -0.1250000000000000000 ) ) ;
#8009=VECTOR ( 'NONE', #3003, 39.37007874015748143 ) ;
#8015=AXIS2_PLACEMENT_3D ( 'NONE', #581, #6167, #463 ) ;
#8019=EDGE_LOOP ( 'NONE', ( #65, #2676, #5820, #6517, #108 ) ) ;
#8031=FACE_OUTER_BOUND ( 'NONE', #2169, .T. ) ;
#8042=DIRECTION ( 'NONE',  ( 0.000000000000000000, 0.000000000000000000, -1.000000000000000000 ) ) ;
#8045=EDGE_LOOP ( 'NONE', ( #7710, #1738, #5149, #4235 ) ) ;
#8047=VERTEX_POINT ( 'NONE', #7677 ) ;
#8048=DIRECTION ( 'NONE',  ( -0.000000000000000000, 0.000000000000000000, 1.000000000000000000 ) ) ;
#8055=AXIS2_PLACEMENT_3D ( 'NONE', #6827, #1176, #2328 ) ;
#8056=CIRCLE ( 'NONE', #4023, 0.2812500000000000555 ) ;
#8061=CARTESIAN_POINT ( 'NONE',  ( -1.763177565995707630, 1.070083551578369763, -0.2959999999999997078 ) ) ;
#8062=VECTOR ( 'NONE', #7901, 39.37007874015748854 ) ;
#8065=ORIENTED_EDGE ( 'NONE', *, *, #5694, .T. ) ;
#8069=ORIENTED_EDGE ( 'NONE', *, *, #5595, .F. ) ;
#8070=CIRCLE ( 'NONE', #4679, 0.4060000000000000830 ) ;
#8077=DIRECTION ( 'NONE',  ( 0.000000000000000000, 0.000000000000000000, -1.000000000000000000 ) ) ;
#8090=EDGE_CURVE ( 'NONE', #2766, #4981, #3947, .T. ) ;
#8091=EDGE_LOOP ( 'NONE', ( #7482, #935, #5988, #155 ) ) ;
#8108=COLOUR_RGB('Light Blue', 0.31764706, 0.68627451, 0.89019608);
#8109=FILL_AREA_STYLE_COLOUR('',#8108);
#8110=FILL_AREA_STYLE('',(#8109));
#8111=SURFACE_STYLE_FILL_AREA(#8110);
#8112=SURFACE_SIDE_STYLE('',(#8111));
#8113=SURFACE_STYLE_USAGE(.BOTH.,#8112);
#8114=PRESENTATION_STYLE_ASSIGNMENT((#8113));
#8136=COLOUR_RGB('Black', 0.09019608, 0.27058824, 0.51372549);
#8137=FILL_AREA_STYLE_COLOUR('',#8136);
#8138=FILL_AREA_STYLE('',(#8137));
#8139=SURFACE_STYLE_FILL_AREA(#8138);
#8140=SURFACE_SIDE_STYLE('',(#8139));
#8141=SURFACE_STYLE_USAGE(.BOTH.,#8140);
#8142=PRESENTATION_STYLE_ASSIGNMENT((#8141));
#8145=STYLED_ITEM('',(#8114),#6445);
#8146=STYLED_ITEM('',(#8142),#6285);
#8147=MECHANICAL_DESIGN_GEOMETRIC_PRESENTATION_REPRESENTATION('',(#8145,#8146),#5783);
ENDSEC;
END-ISO-10303-21;
